ISO-10303-21;
HEADER;
FILE_DESCRIPTION (('STEP AP214'),
    '1' );
FILE_NAME ('END CAP_6266N13.step',
    '2026-10-09T16:01:55',
    ( '' ),
    ( '' ),
    'SwSTEP 2.0',
    'SolidWorks 2024',
    '' );
FILE_SCHEMA (( 'AUTOMOTIVE_DESIGN' ));
ENDSEC;

DATA;
#40=CARTESIAN_POINT ( 'NONE',  ( -12.00000000000000000, -11.18999999999999950, -4.250000000000000000 ) ) ;
#43=FACE_OUTER_BOUND ( 'NONE', #36731, .T. ) ;
#53=DIRECTION ( 'NONE',  ( 0.000000000000000000, -1.000000000000000000, 0.000000000000000000 ) ) ;
#100=AXIS2_PLACEMENT_3D ( 'NONE', #13229, #2981, #46110 ) ;
#112=CARTESIAN_POINT ( 'NONE',  ( 8.249999999999996447, -7.848062532927998269, 0.000000000000000000 ) ) ;
#123=AXIS2_PLACEMENT_3D ( 'NONE', #35895, #68773, #47212 ) ;
#157=DIRECTION ( 'NONE',  ( 1.000000000000000000, 0.000000000000000000, 0.000000000000000000 ) ) ;
#247=DIRECTION ( 'NONE',  ( 0.000000000000000000, 0.000000000000000000, -1.000000000000000000 ) ) ;
#283=CARTESIAN_POINT ( 'NONE',  ( -8.000000000000000000, 8.000000000000000000, -1.000000000000000000 ) ) ;
#304=CARTESIAN_POINT ( 'NONE',  ( 11.18999999999999950, 11.25000000000000178, -5.000000000000000000 ) ) ;
#345=EDGE_CURVE ( 'NONE', #14752, #26669, #26112, .T. ) ;
#376=FACE_OUTER_BOUND ( 'NONE', #48764, .T. ) ;
#465=AXIS2_PLACEMENT_3D ( 'NONE', #49320, #22091, #59913 ) ;
#555=LINE ( 'NONE', #43330, #59554 ) ;
#694=EDGE_CURVE ( 'NONE', #60836, #46781, #44152, .T. ) ;
#721=AXIS2_PLACEMENT_3D ( 'NONE', #41997, #30342, #9477 ) ;
#830=ORIENTED_EDGE ( 'NONE', *, *, #51327, .T. ) ;
#863=CARTESIAN_POINT ( 'NONE',  ( -9.249999999999998224, 8.250000000000001776, 5.000000000000000000 ) ) ;
#871=VECTOR ( 'NONE', #27780, 1000.000000000000000 ) ;
#912=CARTESIAN_POINT ( 'NONE',  ( -7.261609891743268541, -8.000000000000000000, 5.000000000000000000 ) ) ;
#1010=DIRECTION ( 'NONE',  ( -0.000000000000000000, -0.000000000000000000, -1.000000000000000000 ) ) ;
#1017=CARTESIAN_POINT ( 'NONE',  ( -11.19000000000000128, -11.25000000000000000, -5.000000000000000000 ) ) ;
#1047=VERTEX_POINT ( 'NONE', #12389 ) ;
#1171=LINE ( 'NONE', #44978, #64259 ) ;
#1270=DIRECTION ( 'NONE',  ( 1.000000000000000000, 0.000000000000000000, 0.000000000000000000 ) ) ;
#1309=DIRECTION ( 'NONE',  ( 0.000000000000000000, 0.000000000000000000, 1.000000000000000000 ) ) ;
#1458=COLOUR_RGB ( '', 0.09019608, 0.27058824, 0.51372549) ;
#1753=FACE_OUTER_BOUND ( 'NONE', #60046, .T. ) ;
#1827=DIRECTION ( 'NONE',  ( 0.000000000000000000, 0.000000000000000000, 1.000000000000000000 ) ) ;
#1846=AXIS2_PLACEMENT_3D ( 'NONE', #17312, #69696, #65759 ) ;
#1855=VECTOR ( 'NONE', #51255, 1000.000000000000000 ) ;
#1870=CIRCLE ( 'NONE', #41394, 1.000000000000000888 ) ;
#1901=AXIS2_PLACEMENT_3D ( 'NONE', #24715, #9154, #14811 ) ;
#1906=VECTOR ( 'NONE', #11858, 1000.000000000000000 ) ;
#1945=ORIENTED_EDGE ( 'NONE', *, *, #17552, .T. ) ;
#1963=DIRECTION ( 'NONE',  ( -0.000000000000000000, -0.000000000000000000, -1.000000000000000000 ) ) ;
#2170=EDGE_CURVE ( 'NONE', #54089, #37232, #43561, .T. ) ;
#2197=DIRECTION ( 'NONE',  ( -1.000000000000000000, -1.084202172485504434E-16, 0.000000000000000000 ) ) ;
#2297=CARTESIAN_POINT ( 'NONE',  ( 11.18999999999999950, 11.25000000000000178, -4.250000000000000000 ) ) ;
#2300=FACE_OUTER_BOUND ( 'NONE', #60861, .T. ) ;
#2609=ORIENTED_EDGE ( 'NONE', *, *, #69298, .T. ) ;
#2728=EDGE_LOOP ( 'NONE', ( #19936, #57321, #24721, #50943 ) ) ;
#2873=ORIENTED_EDGE ( 'NONE', *, *, #57385, .F. ) ;
#2981=DIRECTION ( 'NONE',  ( 1.000000000000000000, 1.084202172485504434E-16, 0.000000000000000000 ) ) ;
#3103=DIRECTION ( 'NONE',  ( 1.000000000000000000, 0.000000000000000000, 0.000000000000000000 ) ) ;
#3203=ORIENTED_EDGE ( 'NONE', *, *, #12982, .F. ) ;
#3284=CYLINDRICAL_SURFACE ( 'NONE', #16265, 1.000000000000001776 ) ;
#3296=EDGE_CURVE ( 'NONE', #35441, #11801, #21937, .T. ) ;
#3303=CARTESIAN_POINT ( 'NONE',  ( -11.18999999999999950, 11.18999999999999950, -4.250000000000000000 ) ) ;
#3305=EDGE_CURVE ( 'NONE', #46781, #47718, #31982, .T. ) ;
#3366=AXIS2_PLACEMENT_3D ( 'NONE', #66680, #45450, #40505 ) ;
#3374=CARTESIAN_POINT ( 'NONE',  ( -7.261609891743268541, -8.000000000000000000, 0.000000000000000000 ) ) ;
#3381=AXIS2_PLACEMENT_3D ( 'NONE', #44339, #55658, #65913 ) ;
#3409=LINE ( 'NONE', #24977, #36083 ) ;
#3655=ORIENTED_EDGE ( 'NONE', *, *, #40229, .F. ) ;
#3785=DIRECTION ( 'NONE',  ( 1.000000000000000000, 0.000000000000000000, 0.000000000000000000 ) ) ;
#3948=DIRECTION ( 'NONE',  ( 0.000000000000000000, 0.000000000000000000, 1.000000000000000000 ) ) ;
#3956=CARTESIAN_POINT ( 'NONE',  ( -8.249999999999996447, 8.250000000000001776, 0.000000000000000000 ) ) ;
#3966=ORIENTED_EDGE ( 'NONE', *, *, #57121, .T. ) ;
#4069=CARTESIAN_POINT ( 'NONE',  ( 7.261609891743268541, -8.000000000000000000, 5.000000000000000000 ) ) ;
#4189=VERTEX_POINT ( 'NONE', #12224 ) ;
#4242=ORIENTED_EDGE ( 'NONE', *, *, #13850, .F. ) ;
#4294=DIRECTION ( 'NONE',  ( 0.000000000000000000, 0.000000000000000000, 1.000000000000000000 ) ) ;
#4414=TOROIDAL_SURFACE ( 'NONE', #49569, 0.06000000000000080963, 0.7500000000000000000 ) ;
#4426=LINE ( 'NONE', #9361, #47989 ) ;
#4427=FACE_OUTER_BOUND ( 'NONE', #39518, .T. ) ;
#4444=VERTEX_POINT ( 'NONE', #60161 ) ;
#4488=DIRECTION ( 'NONE',  ( -7.751221965937476285E-17, 1.000000000000000000, 0.000000000000000000 ) ) ;
#4504=( LENGTH_UNIT ( ) NAMED_UNIT ( * ) SI_UNIT ( .MILLI., .METRE. ) );
#4533=EDGE_LOOP ( 'NONE', ( #14549, #19404, #15661, #65984, #47333, #34143, #61422, #28531 ) ) ;
#4567=AXIS2_PLACEMENT_3D ( 'NONE', #61571, #54570, #6120 ) ;
#4594=AXIS2_PLACEMENT_3D ( 'NONE', #32061, #41967, #32417 ) ;
#4692=CARTESIAN_POINT ( 'NONE',  ( 8.249999999999996447, -7.848062532927998269, 5.000000000000000000 ) ) ;
#4697=ORIENTED_EDGE ( 'NONE', *, *, #41343, .T. ) ;
#4726=EDGE_CURVE ( 'NONE', #53942, #4894, #68339, .T. ) ;
#4876=ORIENTED_EDGE ( 'NONE', *, *, #44012, .F. ) ;
#4894=VERTEX_POINT ( 'NONE', #60079 ) ;
#5018=ORIENTED_EDGE ( 'NONE', *, *, #31637, .T. ) ;
#5026=FACE_BOUND ( 'NONE', #9818, .T. ) ;
#5158=LINE ( 'NONE', #912, #44840 ) ;
#5367=PLANE ( 'NONE',  #36779 ) ;
#5402=DIRECTION ( 'NONE',  ( -0.000000000000000000, 0.000000000000000000, -1.000000000000000000 ) ) ;
#5450=VERTEX_POINT ( 'NONE', #8328 ) ;
#5526=LINE ( 'NONE', #54658, #871 ) ;
#5569=ORIENTED_EDGE ( 'NONE', *, *, #45750, .F. ) ;
#5581=ORIENTED_EDGE ( 'NONE', *, *, #32046, .T. ) ;
#5731=CARTESIAN_POINT ( 'NONE',  ( 11.25000000000000178, -11.18999999999999950, -5.000000000000000000 ) ) ;
#5741=AXIS2_PLACEMENT_3D ( 'NONE', #3303, #36527, #69406 ) ;
#5846=ORIENTED_EDGE ( 'NONE', *, *, #47282, .F. ) ;
#5927=ORIENTED_EDGE ( 'NONE', *, *, #694, .F. ) ;
#5982=EDGE_CURVE ( 'NONE', #60836, #38359, #30527, .T. ) ;
#6000=ORIENTED_EDGE ( 'NONE', *, *, #3296, .T. ) ;
#6002=ADVANCED_FACE ( 'NONE', ( #30880 ), #46345, .T. ) ;
#6037=AXIS2_PLACEMENT_3D ( 'NONE', #8916, #25551, #36139 ) ;
#6120=DIRECTION ( 'NONE',  ( 1.000000000000000000, 0.000000000000000000, 0.000000000000000000 ) ) ;
#6126=EDGE_CURVE ( 'NONE', #9548, #21103, #41810, .T. ) ;
#6197=ORIENTED_EDGE ( 'NONE', *, *, #69298, .F. ) ;
#6277=CARTESIAN_POINT ( 'NONE',  ( 11.18999999999999950, 11.18999999999999950, -4.250000000000000000 ) ) ;
#6358=CIRCLE ( 'NONE', #51522, 1.000000000000001776 ) ;
#6380=DIRECTION ( 'NONE',  ( 0.000000000000000000, 0.000000000000000000, 1.000000000000000000 ) ) ;
#6498=ORIENTED_EDGE ( 'NONE', *, *, #3296, .F. ) ;
#6606=EDGE_CURVE ( 'NONE', #47718, #38359, #33968, .T. ) ;
#6646=ORIENTED_EDGE ( 'NONE', *, *, #58802, .F. ) ;
#6671=CARTESIAN_POINT ( 'NONE',  ( 11.18999999999999950, 11.18999999999999950, 0.000000000000000000 ) ) ;
#6684=EDGE_CURVE ( 'NONE', #35206, #53942, #24265, .T. ) ;
#6867=DIRECTION ( 'NONE',  ( -1.000000000000000000, 0.000000000000000000, 0.000000000000000000 ) ) ;
#6893=ORIENTED_EDGE ( 'NONE', *, *, #50578, .F. ) ;
#6894=CARTESIAN_POINT ( 'NONE',  ( 7.249999999999995559, 8.250000000000001776, -5.000000000000000000 ) ) ;
#6957=CARTESIAN_POINT ( 'NONE',  ( -12.00000000000000000, -11.18999999999999950, 0.000000000000000000 ) ) ;
#7045=ORIENTED_EDGE ( 'NONE', *, *, #60157, .F. ) ;
#7143=FACE_OUTER_BOUND ( 'NONE', #67127, .T. ) ;
#7154=DIRECTION ( 'NONE',  ( -1.084202172485504434E-16, 1.000000000000000000, 0.000000000000000000 ) ) ;
#7499=CIRCLE ( 'NONE', #10896, 1.000000000000001776 ) ;
#7574=ORIENTED_EDGE ( 'NONE', *, *, #65412, .T. ) ;
#7606=ORIENTED_EDGE ( 'NONE', *, *, #22919, .F. ) ;
#7633=VERTEX_POINT ( 'NONE', #20180 ) ;
#7639=VECTOR ( 'NONE', #49755, 1000.000000000000000 ) ;
#7655=AXIS2_PLACEMENT_3D ( 'NONE', #35496, #19951, #25624 ) ;
#7683=CARTESIAN_POINT ( 'NONE',  ( 8.000000000000000000, 7.281754163448145079, 0.000000000000000000 ) ) ;
#7705=PRODUCT_DEFINITION_CONTEXT ( 'detailed design', #35891, 'design' ) ;
#7778=ORIENTED_EDGE ( 'NONE', *, *, #41448, .T. ) ;
#7890=ORIENTED_EDGE ( 'NONE', *, *, #3305, .T. ) ;
#7908=CARTESIAN_POINT ( 'NONE',  ( -11.19000000000000128, -12.00000000000000000, -4.250000000000000000 ) ) ;
#7912=CARTESIAN_POINT ( 'NONE',  ( 0.000000000000000000, 0.000000000000000000, -1.000000000000000000 ) ) ;
#8016=DIRECTION ( 'NONE',  ( 0.000000000000000000, 0.000000000000000000, 1.000000000000000000 ) ) ;
#8105=EDGE_CURVE ( 'NONE', #56996, #26669, #37316, .T. ) ;
#8223=CARTESIAN_POINT ( 'NONE',  ( -8.249999999999996447, 8.250000000000001776, 0.000000000000000000 ) ) ;
#8239=CIRCLE ( 'NONE', #52324, 1.000000000000000888 ) ;
#8286=CYLINDRICAL_SURFACE ( 'NONE', #56372, 0.8099999999999999423 ) ;
#8294=PLANE ( 'NONE',  #41166 ) ;
#8328=CARTESIAN_POINT ( 'NONE',  ( -11.18999999999999950, 12.00000000000000000, 0.000000000000000000 ) ) ;
#8333=CARTESIAN_POINT ( 'NONE',  ( -12.00000000000000000, 11.18999999999999950, -4.250000000000000000 ) ) ;
#8364=DIRECTION ( 'NONE',  ( -0.000000000000000000, 1.000000000000000000, 0.000000000000000000 ) ) ;
#8382=ORIENTED_EDGE ( 'NONE', *, *, #54030, .F. ) ;
#8481=EDGE_CURVE ( 'NONE', #67890, #37232, #60999, .T. ) ;
#8539=DIRECTION ( 'NONE',  ( -0.000000000000000000, -0.000000000000000000, -1.000000000000000000 ) ) ;
#8568=CIRCLE ( 'NONE', #15412, 0.7500000000000006661 ) ;
#8774=VECTOR ( 'NONE', #55260, 1000.000000000000000 ) ;
#8916=CARTESIAN_POINT ( 'NONE',  ( -11.18999999999999950, -11.18999999999999950, 0.000000000000000000 ) ) ;
#8981=CARTESIAN_POINT ( 'NONE',  ( -7.249999999999995559, -7.848062532927998269, -1.000000000000000000 ) ) ;
#9094=DIRECTION ( 'NONE',  ( 1.000000000000000000, 0.000000000000000000, 0.000000000000000000 ) ) ;
#9101=EDGE_LOOP ( 'NONE', ( #31589, #66443, #22278, #7606 ) ) ;
#9154=DIRECTION ( 'NONE',  ( -0.000000000000000000, -0.000000000000000000, -1.000000000000000000 ) ) ;
#9223=ORIENTED_EDGE ( 'NONE', *, *, #65201, .F. ) ;
#9361=CARTESIAN_POINT ( 'NONE',  ( 8.000000000000001776, -8.000000000000000000, -1.000000000000000000 ) ) ;
#9362=PLANE ( 'NONE',  #56502 ) ;
#9369=EDGE_LOOP ( 'NONE', ( #4697, #47631, #40366, #64002 ) ) ;
#9382=ADVANCED_FACE ( 'NONE', ( #22198 ), #38790, .T. ) ;
#9387=EDGE_CURVE ( 'NONE', #67890, #41002, #60010, .T. ) ;
#9477=DIRECTION ( 'NONE',  ( 1.000000000000000000, 0.000000000000000000, 0.000000000000000000 ) ) ;
#9548=VERTEX_POINT ( 'NONE', #16736 ) ;
#9574=EDGE_LOOP ( 'NONE', ( #42383, #26185 ) ) ;
#9670=AXIS2_PLACEMENT_3D ( 'NONE', #3956, #64071, #67955 ) ;
#9788=PRODUCT_DEFINITION ( 'UNKNOWN', '', #34698, #7705 ) ;
#9795=DIRECTION ( 'NONE',  ( -0.000000000000000000, -0.000000000000000000, -1.000000000000000000 ) ) ;
#9818=EDGE_LOOP ( 'NONE', ( #58424, #59515, #54866, #59126, #40523, #22058, #39873, #31580, #28158, #5927, #58230, #52114, #2873, #29087 ) ) ;
#9819=LINE ( 'NONE', #31020, #48500 ) ;
#9873=ORIENTED_EDGE ( 'NONE', *, *, #34824, .F. ) ;
#9920=EDGE_LOOP ( 'NONE', ( #31883, #27558, #51214, #48086, #24384, #66220, #15203, #36339 ) ) ;
#10076=ORIENTED_EDGE ( 'NONE', *, *, #35912, .T. ) ;
#10078=CARTESIAN_POINT ( 'NONE',  ( 8.249999999999996447, -7.848062532927998269, 0.000000000000000000 ) ) ;
#10126=ADVANCED_FACE ( 'NONE', ( #43 ), #25750, .T. ) ;
#10135=FACE_OUTER_BOUND ( 'NONE', #23558, .T. ) ;
#10170=EDGE_CURVE ( 'NONE', #35206, #62636, #55163, .T. ) ;
#10248=AXIS2_PLACEMENT_3D ( 'NONE', #44383, #49027, #21800 ) ;
#10306=DIRECTION ( 'NONE',  ( -7.751221965937476285E-17, -1.000000000000000000, 0.000000000000000000 ) ) ;
#10344=DIRECTION ( 'NONE',  ( -0.000000000000000000, -0.000000000000000000, -1.000000000000000000 ) ) ;
#10372=CARTESIAN_POINT ( 'NONE',  ( -8.249999999999996447, 8.250000000000001776, -1.000000000000000000 ) ) ;
#10411=DIRECTION ( 'NONE',  ( 0.000000000000000000, 0.000000000000000000, -1.000000000000000000 ) ) ;
#10435=DIRECTION ( 'NONE',  ( -0.000000000000000000, -0.000000000000000000, -1.000000000000000000 ) ) ;
#10481=ORIENTED_EDGE ( 'NONE', *, *, #67959, .T. ) ;
#10635=DIRECTION ( 'NONE',  ( 1.000000000000000000, 0.000000000000000000, 0.000000000000000000 ) ) ;
#10746=DIRECTION ( 'NONE',  ( -0.000000000000000000, -0.000000000000000000, -1.000000000000000000 ) ) ;
#10790=DIRECTION ( 'NONE',  ( 2.312964634635740689E-15, 1.000000000000000000, 0.000000000000000000 ) ) ;
#10896=AXIS2_PLACEMENT_3D ( 'NONE', #65076, #38210, #64041 ) ;
#11071=ORIENTED_EDGE ( 'NONE', *, *, #2170, .F. ) ;
#11084=ORIENTED_EDGE ( 'NONE', *, *, #39431, .F. ) ;
#11125=DIRECTION ( 'NONE',  ( 1.000000000000000000, 0.000000000000000000, 0.000000000000000000 ) ) ;
#11129=ORIENTED_EDGE ( 'NONE', *, *, #39997, .T. ) ;
#11205=FACE_OUTER_BOUND ( 'NONE', #34230, .T. ) ;
#11209=EDGE_LOOP ( 'NONE', ( #38311, #66909, #61375, #69278 ) ) ;
#11307=CIRCLE ( 'NONE', #4567, 0.06000000000000102474 ) ;
#11315=EDGE_LOOP ( 'NONE', ( #45375, #57548, #2609, #32471, #55333, #48344, #5018, #27386 ) ) ;
#11316=CARTESIAN_POINT ( 'NONE',  ( -11.19000000000000128, -12.00000000000000000, 0.000000000000000000 ) ) ;
#11320=EDGE_LOOP ( 'NONE', ( #64700, #27661, #34960, #24360 ) ) ;
#11330=ORIENTED_EDGE ( 'NONE', *, *, #31150, .T. ) ;
#11341=VECTOR ( 'NONE', #9795, 1000.000000000000000 ) ;
#11693=VERTEX_POINT ( 'NONE', #13589 ) ;
#11774=DIRECTION ( 'NONE',  ( 1.000000000000000000, 0.000000000000000000, 0.000000000000000000 ) ) ;
#11801=VERTEX_POINT ( 'NONE', #8981 ) ;
#11841=PLANE ( 'NONE',  #34166 ) ;
#11858=DIRECTION ( 'NONE',  ( 1.000000000000000000, 0.000000000000000000, 0.000000000000000000 ) ) ;
#11928=CARTESIAN_POINT ( 'NONE',  ( 12.00000000000000000, 11.18999999999999950, -5.000000000000000000 ) ) ;
#12224=CARTESIAN_POINT ( 'NONE',  ( 11.25000000000000178, -11.18999999999999950, -5.000000000000000000 ) ) ;
#12248=EDGE_CURVE ( 'NONE', #4189, #4894, #25383, .T. ) ;
#12252=DIRECTION ( 'NONE',  ( 0.000000000000000000, 0.000000000000000000, 1.000000000000000000 ) ) ;
#12389=CARTESIAN_POINT ( 'NONE',  ( 7.281754163448140638, 8.000000000000001776, -1.000000000000000000 ) ) ;
#12535=CARTESIAN_POINT ( 'NONE',  ( 11.18999999999999950, -11.18999999999999950, -5.000000000000000000 ) ) ;
#12553=DIRECTION ( 'NONE',  ( -0.000000000000000000, -0.000000000000000000, -1.000000000000000000 ) ) ;
#12620=DIRECTION ( 'NONE',  ( 1.000000000000000000, 0.000000000000000000, 0.000000000000000000 ) ) ;
#12684=VECTOR ( 'NONE', #37651, 1000.000000000000000 ) ;
#12695=DIRECTION ( 'NONE',  ( 0.000000000000000000, -0.000000000000000000, 1.000000000000000000 ) ) ;
#12744=( GEOMETRIC_REPRESENTATION_CONTEXT ( 3 ) GLOBAL_UNCERTAINTY_ASSIGNED_CONTEXT ( ( #63503 ) ) GLOBAL_UNIT_ASSIGNED_CONTEXT ( ( #4504, #37375, #64588 ) ) REPRESENTATION_CONTEXT ( 'NONE', 'WORKASPACE' ) );
#12765=FACE_OUTER_BOUND ( 'NONE', #11320, .T. ) ;
#12844=AXIS2_PLACEMENT_3D ( 'NONE', #63378, #57365, #48167 ) ;
#12858=FACE_OUTER_BOUND ( 'NONE', #43216, .T. ) ;
#12862=FACE_OUTER_BOUND ( 'NONE', #26436, .T. ) ;
#12939=VECTOR ( 'NONE', #20178, 1000.000000000000000 ) ;
#12982=EDGE_CURVE ( 'NONE', #19489, #51203, #66025, .T. ) ;
#12994=EDGE_CURVE ( 'NONE', #57047, #22012, #22901, .T. ) ;
#13167=CARTESIAN_POINT ( 'NONE',  ( 8.249999999999996447, -7.848062532927998269, -1.000000000000000000 ) ) ;
#13229=CARTESIAN_POINT ( 'NONE',  ( 8.000000000000001776, -8.000000000000000000, -1.000000000000000000 ) ) ;
#13236=DIRECTION ( 'NONE',  ( -0.000000000000000000, -0.000000000000000000, -1.000000000000000000 ) ) ;
#13340=LINE ( 'NONE', #67081, #57725 ) ;
#13589=CARTESIAN_POINT ( 'NONE',  ( 12.00000000000000178, -11.18999999999999950, -4.250000000000000000 ) ) ;
#13647=ORIENTED_EDGE ( 'NONE', *, *, #39134, .F. ) ;
#13746=EDGE_LOOP ( 'NONE', ( #21987, #36631, #56829, #4876 ) ) ;
#13850=EDGE_CURVE ( 'NONE', #21103, #38962, #29685, .T. ) ;
#14255=EDGE_CURVE ( 'NONE', #11801, #41002, #45914, .T. ) ;
#14323=ORIENTED_EDGE ( 'NONE', *, *, #13850, .T. ) ;
#14325=FACE_OUTER_BOUND ( 'NONE', #45221, .T. ) ;
#14366=CARTESIAN_POINT ( 'NONE',  ( 11.25000000000000178, 11.18999999999999950, -5.000000000000000000 ) ) ;
#14446=ORIENTED_EDGE ( 'NONE', *, *, #43607, .T. ) ;
#14451=ORIENTED_EDGE ( 'NONE', *, *, #31637, .F. ) ;
#14549=ORIENTED_EDGE ( 'NONE', *, *, #26124, .T. ) ;
#14554=CARTESIAN_POINT ( 'NONE',  ( 11.18999999999999950, -11.18999999999999950, -5.000000000000000000 ) ) ;
#14664=DIRECTION ( 'NONE',  ( 0.000000000000000000, -0.000000000000000000, -1.000000000000000000 ) ) ;
#14693=ORIENTED_EDGE ( 'NONE', *, *, #8481, .T. ) ;
#14723=VECTOR ( 'NONE', #12553, 1000.000000000000000 ) ;
#14752=VERTEX_POINT ( 'NONE', #67365 ) ;
#14811=DIRECTION ( 'NONE',  ( -1.000000000000000000, 0.000000000000000000, 0.000000000000000000 ) ) ;
#14933=CARTESIAN_POINT ( 'NONE',  ( 11.18999999999999950, 12.00000000000000178, -4.250000000000000000 ) ) ;
#14939=AXIS2_PLACEMENT_3D ( 'NONE', #54343, #44742, #247 ) ;
#14969=DIRECTION ( 'NONE',  ( -0.000000000000000000, -0.000000000000000000, -1.000000000000000000 ) ) ;
#15015=DIRECTION ( 'NONE',  ( -0.000000000000000000, -0.000000000000000000, -1.000000000000000000 ) ) ;
#15112=VERTEX_POINT ( 'NONE', #40 ) ;
#15140=SHAPE_DEFINITION_REPRESENTATION ( #55550, #60228 ) ;
#15185=AXIS2_PLACEMENT_3D ( 'NONE', #49290, #27707, #11774 ) ;
#15203=ORIENTED_EDGE ( 'NONE', *, *, #29934, .T. ) ;
#15412=AXIS2_PLACEMENT_3D ( 'NONE', #42972, #33056, #10790 ) ;
#15428=DIRECTION ( 'NONE',  ( -0.000000000000000000, -0.000000000000000000, -1.000000000000000000 ) ) ;
#15465=SURFACE_STYLE_FILL_AREA ( #47977 ) ;
#15587=CARTESIAN_POINT ( 'NONE',  ( 11.19000000000000128, -11.25000000000000000, -4.250000000000000000 ) ) ;
#15644=LINE ( 'NONE', #5731, #67118 ) ;
#15661=ORIENTED_EDGE ( 'NONE', *, *, #12248, .T. ) ;
#15699=CARTESIAN_POINT ( 'NONE',  ( -9.249999999999998224, -7.848062532927998269, -5.000000000000000000 ) ) ;
#15758=VERTEX_POINT ( 'NONE', #50114 ) ;
#16021=VECTOR ( 'NONE', #60125, 1000.000000000000000 ) ;
#16075=EDGE_CURVE ( 'NONE', #30509, #9548, #5526, .T. ) ;
#16081=CARTESIAN_POINT ( 'NONE',  ( 11.18999999999999950, 12.00000000000000178, -5.000000000000000000 ) ) ;
#16106=EDGE_CURVE ( 'NONE', #53942, #11693, #30221, .T. ) ;
#16217=VERTEX_POINT ( 'NONE', #35778 ) ;
#16258=AXIS2_PLACEMENT_3D ( 'NONE', #21372, #26329, #31992 ) ;
#16265=AXIS2_PLACEMENT_3D ( 'NONE', #4692, #10344, #47127 ) ;
#16266=CIRCLE ( 'NONE', #55622, 1.000000000000000888 ) ;
#16398=ORIENTED_EDGE ( 'NONE', *, *, #3305, .F. ) ;
#16415=ORIENTED_EDGE ( 'NONE', *, *, #51817, .T. ) ;
#16418=AXIS2_PLACEMENT_3D ( 'NONE', #48407, #53719, #69971 ) ;
#16561=ORIENTED_EDGE ( 'NONE', *, *, #65586, .F. ) ;
#16652=ORIENTED_EDGE ( 'NONE', *, *, #47282, .T. ) ;
#16736=CARTESIAN_POINT ( 'NONE',  ( -8.000000000000000000, -6.879816696376141572, 0.000000000000000000 ) ) ;
#16787=SHAPE_REPRESENTATION_RELATIONSHIP ( 'NONE' , 'NONE' ,  #60228, #36842 ) ;
#16818=EDGE_CURVE ( 'NONE', #4894, #7633, #37799, .T. ) ;
#17163=DIRECTION ( 'NONE',  ( 1.000000000000000000, 0.000000000000000000, 0.000000000000000000 ) ) ;
#17222=FACE_OUTER_BOUND ( 'NONE', #26685, .T. ) ;
#17312=CARTESIAN_POINT ( 'NONE',  ( -11.18999999999999950, 11.18999999999999950, -5.000000000000000000 ) ) ;
#17322=CIRCLE ( 'NONE', #6037, 0.8099999999999999423 ) ;
#17366=EDGE_CURVE ( 'NONE', #35441, #57821, #40479, .T. ) ;
#17375=CARTESIAN_POINT ( 'NONE',  ( -7.281754163448141526, 8.000000000000000000, 5.000000000000000000 ) ) ;
#17421=LINE ( 'NONE', #32656, #8774 ) ;
#17499=ADVANCED_FACE ( 'NONE', ( #41540 ), #8294, .T. ) ;
#17523=CARTESIAN_POINT ( 'NONE',  ( 8.000000000000000000, 7.281754163448145079, 5.000000000000000000 ) ) ;
#17547=VERTEX_POINT ( 'NONE', #46136 ) ;
#17552=EDGE_CURVE ( 'NONE', #52724, #34676, #4426, .T. ) ;
#17568=DIRECTION ( 'NONE',  ( 1.000000000000000000, 0.000000000000000000, 0.000000000000000000 ) ) ;
#17663=CARTESIAN_POINT ( 'NONE',  ( -7.261609891743268541, -8.000000000000000000, -1.000000000000000000 ) ) ;
#17722=PRODUCT ( 'END CAP_6266N13', 'END CAP_6266N13', '', ( #37409 ) ) ;
#17750=CARTESIAN_POINT ( 'NONE',  ( -11.19000000000000128, -11.25000000000000000, -4.250000000000000000 ) ) ;
#18010=DIRECTION ( 'NONE',  ( 0.000000000000000000, 1.000000000000000000, 0.000000000000000000 ) ) ;
#18214=DIRECTION ( 'NONE',  ( -1.000000000000000000, 0.000000000000000000, 0.000000000000000000 ) ) ;
#18369=VECTOR ( 'NONE', #15015, 1000.000000000000000 ) ;
#18414=DIRECTION ( 'NONE',  ( -1.000000000000000000, -0.000000000000000000, -0.000000000000000000 ) ) ;
#18422=DIRECTION ( 'NONE',  ( -1.000000000000000000, 0.000000000000000000, 0.000000000000000000 ) ) ;
#18445=DIRECTION ( 'NONE',  ( -0.000000000000000000, -0.000000000000000000, -1.000000000000000000 ) ) ;
#18448=CIRCLE ( 'NONE', #26256, 1.000000000000001776 ) ;
#18593=VERTEX_POINT ( 'NONE', #50413 ) ;
#18764=CARTESIAN_POINT ( 'NONE',  ( -8.000000000000000000, 7.281754163448145079, -1.000000000000000000 ) ) ;
#18991=CARTESIAN_POINT ( 'NONE',  ( 11.18999999999999950, -11.18999999999999950, -4.250000000000000000 ) ) ;
#19051=CIRCLE ( 'NONE', #42786, 0.06000000000000102474 ) ;
#19056=CIRCLE ( 'NONE', #62004, 1.000000000000000888 ) ;
#19244=FACE_OUTER_BOUND ( 'NONE', #2728, .T. ) ;
#19245=AXIS2_PLACEMENT_3D ( 'NONE', #65159, #42877, #66773 ) ;
#19359=AXIS2_PLACEMENT_3D ( 'NONE', #41802, #36872, #63379 ) ;
#19383=DIRECTION ( 'NONE',  ( -1.000000000000000000, 0.000000000000000000, -0.000000000000000000 ) ) ;
#19404=ORIENTED_EDGE ( 'NONE', *, *, #66701, .T. ) ;
#19459=VECTOR ( 'NONE', #59829, 1000.000000000000000 ) ;
#19463=EDGE_LOOP ( 'NONE', ( #21635, #9873 ) ) ;
#19489=VERTEX_POINT ( 'NONE', #62438 ) ;
#19609=DIRECTION ( 'NONE',  ( -1.084202172485504434E-16, 1.000000000000000000, 0.000000000000000000 ) ) ;
#19719=ORIENTED_EDGE ( 'NONE', *, *, #61767, .T. ) ;
#19812=ADVANCED_FACE ( 'NONE', ( #19244 ), #61314, .F. ) ;
#19815=LINE ( 'NONE', #25488, #12939 ) ;
#19827=FACE_OUTER_BOUND ( 'NONE', #32069, .T. ) ;
#19896=FACE_OUTER_BOUND ( 'NONE', #33246, .T. ) ;
#19936=ORIENTED_EDGE ( 'NONE', *, *, #63468, .F. ) ;
#19951=DIRECTION ( 'NONE',  ( 0.000000000000000000, 0.000000000000000000, 1.000000000000000000 ) ) ;
#20041=DIRECTION ( 'NONE',  ( 0.000000000000000000, 0.000000000000000000, 1.000000000000000000 ) ) ;
#20108=ADVANCED_FACE ( 'NONE', ( #7143 ), #34355, .F. ) ;
#20178=DIRECTION ( 'NONE',  ( 0.000000000000000000, 0.000000000000000000, 1.000000000000000000 ) ) ;
#20180=CARTESIAN_POINT ( 'NONE',  ( -11.18999999999999950, -11.25000000000000000, -5.000000000000000000 ) ) ;
#20204=CARTESIAN_POINT ( 'NONE',  ( -12.00000000000000000, 11.18999999999999950, 0.000000000000000000 ) ) ;
#20270=DIRECTION ( 'NONE',  ( 1.000000000000000000, 0.000000000000000000, 0.000000000000000000 ) ) ;
#20319=CARTESIAN_POINT ( 'NONE',  ( 8.249999999999996447, 8.250000000000001776, 5.000000000000000000 ) ) ;
#20410=VECTOR ( 'NONE', #51132, 1000.000000000000000 ) ;
#20461=CYLINDRICAL_SURFACE ( 'NONE', #1901, 1.000000000000000888 ) ;
#20774=VECTOR ( 'NONE', #10746, 1000.000000000000000 ) ;
#20826=DIRECTION ( 'NONE',  ( -7.751221965937476285E-17, -1.000000000000000000, 0.000000000000000000 ) ) ;
#20907=ORIENTED_EDGE ( 'NONE', *, *, #39997, .F. ) ;
#20938=VECTOR ( 'NONE', #34536, 1000.000000000000000 ) ;
#21103=VERTEX_POINT ( 'NONE', #21707 ) ;
#21113=ORIENTED_EDGE ( 'NONE', *, *, #51327, .F. ) ;
#21136=ORIENTED_EDGE ( 'NONE', *, *, #57659, .T. ) ;
#21179=ADVANCED_FACE ( 'NONE', ( #34363 ), #51711, .F. ) ;
#21372=CARTESIAN_POINT ( 'NONE',  ( 8.249999999999996447, 8.250000000000001776, 0.000000000000000000 ) ) ;
#21480=ORIENTED_EDGE ( 'NONE', *, *, #46694, .F. ) ;
#21635=ORIENTED_EDGE ( 'NONE', *, *, #6606, .F. ) ;
#21707=CARTESIAN_POINT ( 'NONE',  ( -9.249999999999998224, -7.848062532927998269, 0.000000000000000000 ) ) ;
#21799=SURFACE_SIDE_STYLE ('',( #15465 ) ) ;
#21800=DIRECTION ( 'NONE',  ( 1.000000000000000000, 0.000000000000000000, 0.000000000000000000 ) ) ;
#21803=VERTEX_POINT ( 'NONE', #7683 ) ;
#21861=VECTOR ( 'NONE', #18414, 1000.000000000000000 ) ;
#21937=CIRCLE ( 'NONE', #15185, 1.000000000000001776 ) ;
#21987=ORIENTED_EDGE ( 'NONE', *, *, #59894, .T. ) ;
#22012=VERTEX_POINT ( 'NONE', #56823 ) ;
#22058=ORIENTED_EDGE ( 'NONE', *, *, #60831, .F. ) ;
#22091=DIRECTION ( 'NONE',  ( 0.000000000000000000, 0.000000000000000000, 1.000000000000000000 ) ) ;
#22198=FACE_OUTER_BOUND ( 'NONE', #52808, .T. ) ;
#22199=CARTESIAN_POINT ( 'NONE',  ( 7.281754163448140638, 8.000000000000001776, 5.000000000000000000 ) ) ;
#22223=DIRECTION ( 'NONE',  ( -0.000000000000000000, -0.000000000000000000, -1.000000000000000000 ) ) ;
#22278=ORIENTED_EDGE ( 'NONE', *, *, #55539, .T. ) ;
#22442=( NAMED_UNIT ( * ) PLANE_ANGLE_UNIT ( ) SI_UNIT ( $, .RADIAN. ) );
#22775=CARTESIAN_POINT ( 'NONE',  ( 0.000000000000000000, 0.000000000000000000, 0.000000000000000000 ) ) ;
#22901=LINE ( 'NONE', #11928, #20938 ) ;
#22919=EDGE_CURVE ( 'NONE', #62636, #43565, #55697, .T. ) ;
#23113=( LENGTH_UNIT ( ) NAMED_UNIT ( * ) SI_UNIT ( .MILLI., .METRE. ) );
#23117=ORIENTED_EDGE ( 'NONE', *, *, #66701, .F. ) ;
#23164=DIRECTION ( 'NONE',  ( 1.000000000000000000, 0.000000000000000000, 0.000000000000000000 ) ) ;
#23222=ADVANCED_FACE ( 'NONE', ( #53551 ), #69453, .T. ) ;
#23327=PLANE ( 'NONE',  #25065 ) ;
#23435=DIRECTION ( 'NONE',  ( -1.000000000000000000, -1.084202172485504434E-16, 0.000000000000000000 ) ) ;
#23442=AXIS2_PLACEMENT_3D ( 'NONE', #46388, #7154, #23435 ) ;
#23558=EDGE_LOOP ( 'NONE', ( #31416, #45995, #42623, #41411 ) ) ;
#23588=CARTESIAN_POINT ( 'NONE',  ( 11.18999999999999950, 11.18999999999999950, -4.250000000000000000 ) ) ;
#23654=ORIENTED_EDGE ( 'NONE', *, *, #14255, .F. ) ;
#23722=ORIENTED_EDGE ( 'NONE', *, *, #17366, .T. ) ;
#23773=VECTOR ( 'NONE', #14969, 1000.000000000000000 ) ;
#23811=EDGE_CURVE ( 'NONE', #15112, #49163, #44924, .T. ) ;
#23859=DIRECTION ( 'NONE',  ( 0.000000000000000000, 0.000000000000000000, -1.000000000000000000 ) ) ;
#23869=LINE ( 'NONE', #45426, #27431 ) ;
#24007=ORIENTED_EDGE ( 'NONE', *, *, #65412, .F. ) ;
#24012=VECTOR ( 'NONE', #62650, 1000.000000000000000 ) ;
#24111=CARTESIAN_POINT ( 'NONE',  ( -8.249999999999996447, -7.848062532927998269, 5.000000000000000000 ) ) ;
#24147=DIRECTION ( 'NONE',  ( 1.000000000000000000, 0.000000000000000000, 0.000000000000000000 ) ) ;
#24189=PLANE ( 'NONE',  #51542 ) ;
#24265=LINE ( 'NONE', #34513, #20410 ) ;
#24295=DIRECTION ( 'NONE',  ( 0.000000000000000000, 0.000000000000000000, 1.000000000000000000 ) ) ;
#24360=ORIENTED_EDGE ( 'NONE', *, *, #6684, .F. ) ;
#24384=ORIENTED_EDGE ( 'NONE', *, *, #57385, .T. ) ;
#24652=CARTESIAN_POINT ( 'NONE',  ( -9.249999999999998224, 8.250000000000001776, -5.000000000000000000 ) ) ;
#24715=CARTESIAN_POINT ( 'NONE',  ( -8.249999999999996447, 8.250000000000001776, 5.000000000000000000 ) ) ;
#24721=ORIENTED_EDGE ( 'NONE', *, *, #44744, .T. ) ;
#24873=CARTESIAN_POINT ( 'NONE',  ( -7.249999999999995559, 8.250000000000001776, 5.000000000000000000 ) ) ;
#24909=EDGE_CURVE ( 'NONE', #64954, #58759, #19056, .T. ) ;
#24943=ORIENTED_EDGE ( 'NONE', *, *, #55883, .F. ) ;
#24977=CARTESIAN_POINT ( 'NONE',  ( -11.18999999999999950, 12.00000000000000000, -5.000000000000000000 ) ) ;
#25065=AXIS2_PLACEMENT_3D ( 'NONE', #66458, #18010, #12695 ) ;
#25092=VECTOR ( 'NONE', #20826, 1000.000000000000000 ) ;
#25102=EDGE_LOOP ( 'NONE', ( #58279, #34740, #29098, #36266 ) ) ;
#25383=CIRCLE ( 'NONE', #28790, 0.06000000000000102474 ) ;
#25384=CIRCLE ( 'NONE', #49105, 0.7499999999999997780 ) ;
#25448=CARTESIAN_POINT ( 'NONE',  ( -9.249999999999998224, -7.848062532927998269, 5.000000000000000000 ) ) ;
#25488=CARTESIAN_POINT ( 'NONE',  ( -12.00000000000000000, 11.18999999999999950, -5.000000000000000000 ) ) ;
#25516=VECTOR ( 'NONE', #59003, 1000.000000000000000 ) ;
#25551=DIRECTION ( 'NONE',  ( 0.000000000000000000, 0.000000000000000000, 1.000000000000000000 ) ) ;
#25556=PLANE ( 'NONE',  #12844 ) ;
#25558=ORIENTED_EDGE ( 'NONE', *, *, #51817, .F. ) ;
#25624=DIRECTION ( 'NONE',  ( 1.000000000000000000, 0.000000000000000000, 0.000000000000000000 ) ) ;
#25750=TOROIDAL_SURFACE ( 'NONE', #62985, 0.06000000000000080963, 0.7500000000000000000 ) ;
#25755=( GEOMETRIC_REPRESENTATION_CONTEXT ( 3 ) GLOBAL_UNCERTAINTY_ASSIGNED_CONTEXT ( ( #69146 ) ) GLOBAL_UNIT_ASSIGNED_CONTEXT ( ( #23113, #22442, #65240 ) ) REPRESENTATION_CONTEXT ( 'NONE', 'WORKASPACE' ) );
#25765=ADVANCED_FACE ( 'NONE', ( #11205 ), #59655, .T. ) ;
#25900=EDGE_CURVE ( 'NONE', #58759, #64954, #33827, .T. ) ;
#25996=ORIENTED_EDGE ( 'NONE', *, *, #66614, .T. ) ;
#26017=ORIENTED_EDGE ( 'NONE', *, *, #41448, .F. ) ;
#26049=CARTESIAN_POINT ( 'NONE',  ( -11.25000000000000000, 11.18999999999999950, -5.000000000000000000 ) ) ;
#26112=CIRCLE ( 'NONE', #123, 0.8099999999999999423 ) ;
#26124=EDGE_CURVE ( 'NONE', #52731, #34737, #19051, .T. ) ;
#26185=ORIENTED_EDGE ( 'NONE', *, *, #25900, .F. ) ;
#26256=AXIS2_PLACEMENT_3D ( 'NONE', #32843, #37465, #53729 ) ;
#26329=DIRECTION ( 'NONE',  ( 0.000000000000000000, 0.000000000000000000, 1.000000000000000000 ) ) ;
#26413=FILL_AREA_STYLE_COLOUR ( '', #1458 ) ;
#26436=EDGE_LOOP ( 'NONE', ( #10481, #40534, #29807, #5581 ) ) ;
#26528=DIRECTION ( 'NONE',  ( 1.000000000000000000, 0.000000000000000000, 0.000000000000000000 ) ) ;
#26551=CYLINDRICAL_SURFACE ( 'NONE', #1846, 0.8099999999999999423 ) ;
#26669=VERTEX_POINT ( 'NONE', #8333 ) ;
#26677=EDGE_LOOP ( 'NONE', ( #43963, #55628 ) ) ;
#26685=EDGE_LOOP ( 'NONE', ( #44640, #39441, #25558, #61370 ) ) ;
#26690=AXIS2_PLACEMENT_3D ( 'NONE', #24111, #18445, #29762 ) ;
#26769=EDGE_LOOP ( 'NONE', ( #44185, #46602, #7890, #28737 ) ) ;
#26847=FACE_OUTER_BOUND ( 'NONE', #41989, .T. ) ;
#26860=VECTOR ( 'NONE', #29345, 1000.000000000000000 ) ;
#26921=ORIENTED_EDGE ( 'NONE', *, *, #49285, .T. ) ;
#26923=DIRECTION ( 'NONE',  ( 0.000000000000000000, -0.000000000000000000, -1.000000000000000000 ) ) ;
#26925=CIRCLE ( 'NONE', #7655, 1.000000000000000888 ) ;
#27252=ORIENTED_EDGE ( 'NONE', *, *, #60429, .T. ) ;
#27260=CIRCLE ( 'NONE', #4594, 1.000000000000001776 ) ;
#27377=ADVANCED_FACE ( 'NONE', ( #12765 ), #50964, .T. ) ;
#27386=ORIENTED_EDGE ( 'NONE', *, *, #22919, .T. ) ;
#27431=VECTOR ( 'NONE', #66999, 1000.000000000000000 ) ;
#27558=ORIENTED_EDGE ( 'NONE', *, *, #63468, .T. ) ;
#27661=ORIENTED_EDGE ( 'NONE', *, *, #16818, .F. ) ;
#27707=DIRECTION ( 'NONE',  ( 0.000000000000000000, 0.000000000000000000, 1.000000000000000000 ) ) ;
#27739=CARTESIAN_POINT ( 'NONE',  ( 11.18999999999999950, 11.18999999999999950, -5.000000000000000000 ) ) ;
#27780=DIRECTION ( 'NONE',  ( 0.000000000000000000, -1.000000000000000000, 0.000000000000000000 ) ) ;
#27848=DIRECTION ( 'NONE',  ( 0.000000000000000000, 0.000000000000000000, 1.000000000000000000 ) ) ;
#28123=FACE_BOUND ( 'NONE', #9574, .T. ) ;
#28127=DIRECTION ( 'NONE',  ( 0.000000000000000000, 0.000000000000000000, 1.000000000000000000 ) ) ;
#28158=ORIENTED_EDGE ( 'NONE', *, *, #60896, .F. ) ;
#28169=ORIENTED_EDGE ( 'NONE', *, *, #12994, .F. ) ;
#28187=ADVANCED_FACE ( 'NONE', ( #12862 ), #45396, .F. ) ;
#28237=VECTOR ( 'NONE', #66668, 1000.000000000000000 ) ;
#28242=AXIS2_PLACEMENT_3D ( 'NONE', #39771, #1963, #18214 ) ;
#28531=ORIENTED_EDGE ( 'NONE', *, *, #44012, .T. ) ;
#28623=DIRECTION ( 'NONE',  ( 0.000000000000000000, 0.000000000000000000, 1.000000000000000000 ) ) ;
#28737=ORIENTED_EDGE ( 'NONE', *, *, #6606, .T. ) ;
#28766=AXIS2_PLACEMENT_3D ( 'NONE', #31374, #52939, #4488 ) ;
#28790=AXIS2_PLACEMENT_3D ( 'NONE', #14554, #8539, #52395 ) ;
#28859=CARTESIAN_POINT ( 'NONE',  ( -8.249999999999996447, 8.250000000000001776, -5.000000000000000000 ) ) ;
#29065=ADVANCED_FACE ( 'NONE', ( #1753 ), #23327, .T. ) ;
#29075=VECTOR ( 'NONE', #47605, 1000.000000000000000 ) ;
#29087=ORIENTED_EDGE ( 'NONE', *, *, #66315, .F. ) ;
#29098=ORIENTED_EDGE ( 'NONE', *, *, #44269, .F. ) ;
#29140=EDGE_LOOP ( 'NONE', ( #68347, #11129, #7778, #3203, #7574, #39653 ) ) ;
#29243=DIRECTION ( 'NONE',  ( 0.000000000000000000, 0.000000000000000000, 1.000000000000000000 ) ) ;
#29248=CIRCLE ( 'NONE', #37173, 0.8099999999999999423 ) ;
#29345=DIRECTION ( 'NONE',  ( 0.000000000000000000, 0.000000000000000000, 1.000000000000000000 ) ) ;
#29381=CARTESIAN_POINT ( 'NONE',  ( -11.18999999999999950, 12.00000000000000178, 0.000000000000000000 ) ) ;
#29488=DIRECTION ( 'NONE',  ( 0.000000000000000000, 0.000000000000000000, 1.000000000000000000 ) ) ;
#29685=LINE ( 'NONE', #25448, #1855 ) ;
#29732=LINE ( 'NONE', #29381, #21861 ) ;
#29762=DIRECTION ( 'NONE',  ( -1.000000000000000000, 0.000000000000000000, 0.000000000000000000 ) ) ;
#29770=CARTESIAN_POINT ( 'NONE',  ( 11.18999999999999950, -11.18999999999999950, -4.250000000000000000 ) ) ;
#29788=ADVANCED_FACE ( 'NONE', ( #28123, #44361, #43694, #61319, #34442 ), #11841, .F. ) ;
#29807=ORIENTED_EDGE ( 'NONE', *, *, #17552, .F. ) ;
#29864=CARTESIAN_POINT ( 'NONE',  ( 11.18999999999999950, -11.18999999999999950, -5.000000000000000000 ) ) ;
#29934=EDGE_CURVE ( 'NONE', #1047, #34676, #8239, .T. ) ;
#30096=ADVANCED_FACE ( 'NONE', ( #33653 ), #60860, .F. ) ;
#30139=DIRECTION ( 'NONE',  ( 0.000000000000000000, 0.000000000000000000, 1.000000000000000000 ) ) ;
#30219=ORIENTED_EDGE ( 'NONE', *, *, #60896, .T. ) ;
#30221=CIRCLE ( 'NONE', #34691, 0.8099999999999999423 ) ;
#30342=DIRECTION ( 'NONE',  ( 7.751221965937476285E-17, -1.000000000000000000, 0.000000000000000000 ) ) ;
#30458=ORIENTED_EDGE ( 'NONE', *, *, #6126, .T. ) ;
#30494=DIRECTION ( 'NONE',  ( -0.000000000000000000, 0.000000000000000000, -1.000000000000000000 ) ) ;
#30509=VERTEX_POINT ( 'NONE', #38490 ) ;
#30527=LINE ( 'NONE', #24873, #23773 ) ;
#30600=ORIENTED_EDGE ( 'NONE', *, *, #5982, .T. ) ;
#30780=DIRECTION ( 'NONE',  ( -1.084202172485504434E-16, 1.000000000000000000, 0.000000000000000000 ) ) ;
#30880=FACE_OUTER_BOUND ( 'NONE', #11209, .T. ) ;
#30903=CARTESIAN_POINT ( 'NONE',  ( -7.249999999999995559, -7.848062532927998269, -5.000000000000000000 ) ) ;
#31020=CARTESIAN_POINT ( 'NONE',  ( 8.000000000000001776, -6.879816696376140683, 5.000000000000000000 ) ) ;
#31072=FACE_OUTER_BOUND ( 'NONE', #26769, .T. ) ;
#31150=EDGE_CURVE ( 'NONE', #59678, #54089, #23869, .T. ) ;
#31168=EDGE_CURVE ( 'NONE', #4444, #57821, #52499, .T. ) ;
#31180=CARTESIAN_POINT ( 'NONE',  ( 8.249999999999996447, -7.848062532927998269, -1.000000000000000000 ) ) ;
#31279=ORIENTED_EDGE ( 'NONE', *, *, #16106, .T. ) ;
#31289=CARTESIAN_POINT ( 'NONE',  ( 7.249999999999995559, 8.250000000000001776, 5.000000000000000000 ) ) ;
#31374=CARTESIAN_POINT ( 'NONE',  ( 12.00000000000000000, 11.18999999999999950, -5.000000000000000000 ) ) ;
#31388=PRESENTATION_STYLE_ASSIGNMENT (( #37037 ) ) ;
#31416=ORIENTED_EDGE ( 'NONE', *, *, #32382, .F. ) ;
#31493=CARTESIAN_POINT ( 'NONE',  ( 8.000000000000001776, -8.000000000000000000, 0.000000000000000000 ) ) ;
#31569=CARTESIAN_POINT ( 'NONE',  ( 8.249999999999996447, 8.250000000000001776, -5.000000000000000000 ) ) ;
#31580=ORIENTED_EDGE ( 'NONE', *, *, #16075, .F. ) ;
#31589=ORIENTED_EDGE ( 'NONE', *, *, #10170, .F. ) ;
#31637=EDGE_CURVE ( 'NONE', #49163, #62636, #17322, .T. ) ;
#31790=CYLINDRICAL_SURFACE ( 'NONE', #69731, 1.000000000000001776 ) ;
#31883=ORIENTED_EDGE ( 'NONE', *, *, #47027, .T. ) ;
#31982=LINE ( 'NONE', #863, #20774 ) ;
#31992=DIRECTION ( 'NONE',  ( 1.000000000000000000, 0.000000000000000000, 0.000000000000000000 ) ) ;
#32046=EDGE_CURVE ( 'NONE', #52724, #18593, #9819, .T. ) ;
#32061=CARTESIAN_POINT ( 'NONE',  ( 8.249999999999996447, -7.848062532927998269, -5.000000000000000000 ) ) ;
#32069=EDGE_LOOP ( 'NONE', ( #44558, #830, #49561, #14451 ) ) ;
#32118=ORIENTED_EDGE ( 'NONE', *, *, #39134, .T. ) ;
#32151=VECTOR ( 'NONE', #1270, 1000.000000000000000 ) ;
#32355=DIRECTION ( 'NONE',  ( 1.000000000000000000, 0.000000000000000000, 0.000000000000000000 ) ) ;
#32382=EDGE_CURVE ( 'NONE', #11693, #16217, #40488, .T. ) ;
#32417=DIRECTION ( 'NONE',  ( -1.000000000000000000, 0.000000000000000000, 0.000000000000000000 ) ) ;
#32443=CARTESIAN_POINT ( 'NONE',  ( -11.25000000000000000, 11.18999999999999950, -4.250000000000000000 ) ) ;
#32449=EDGE_CURVE ( 'NONE', #4444, #48626, #37296, .T. ) ;
#32471=ORIENTED_EDGE ( 'NONE', *, *, #65201, .T. ) ;
#32627=EDGE_LOOP ( 'NONE', ( #41488, #26017 ) ) ;
#32634=DIRECTION ( 'NONE',  ( 0.000000000000000000, 0.000000000000000000, 1.000000000000000000 ) ) ;
#32656=CARTESIAN_POINT ( 'NONE',  ( -7.249999999999995559, -7.848062532927998269, 5.000000000000000000 ) ) ;
#32842=ADVANCED_FACE ( 'NONE', ( #19896 ), #3284, .F. ) ;
#32843=CARTESIAN_POINT ( 'NONE',  ( -8.249999999999996447, -7.848062532927998269, -5.000000000000000000 ) ) ;
#33056=DIRECTION ( 'NONE',  ( 1.000000000000000000, -2.312964634635741083E-15, 5.349805401075652267E-30 ) ) ;
#33246=EDGE_LOOP ( 'NONE', ( #20907, #27252, #65299, #52030, #46251, #19719 ) ) ;
#33304=ORIENTED_EDGE ( 'NONE', *, *, #59592, .T. ) ;
#33327=CIRCLE ( 'NONE', #51383, 0.7499999999999997780 ) ;
#33414=DIRECTION ( 'NONE',  ( 0.000000000000000000, 0.000000000000000000, -1.000000000000000000 ) ) ;
#33431=DIRECTION ( 'NONE',  ( 0.000000000000000000, 0.000000000000000000, 1.000000000000000000 ) ) ;
#33471=DIRECTION ( 'NONE',  ( -1.000000000000000000, 0.000000000000000000, 0.000000000000000000 ) ) ;
#33482=LINE ( 'NONE', #49742, #66095 ) ;
#33546=CIRCLE ( 'NONE', #64074, 1.000000000000001776 ) ;
#33587=CARTESIAN_POINT ( 'NONE',  ( -11.18999999999999950, -11.18999999999999950, -4.250000000000000000 ) ) ;
#33653=FACE_OUTER_BOUND ( 'NONE', #67953, .T. ) ;
#33827=CIRCLE ( 'NONE', #3366, 1.000000000000000888 ) ;
#33968=CIRCLE ( 'NONE', #43017, 1.000000000000000888 ) ;
#33984=CARTESIAN_POINT ( 'NONE',  ( -8.000000000000000000, 8.000000000000000000, -1.000000000000000000 ) ) ;
#34143=ORIENTED_EDGE ( 'NONE', *, *, #46694, .T. ) ;
#34160=DIRECTION ( 'NONE',  ( -1.000000000000000000, 0.000000000000000000, 0.000000000000000000 ) ) ;
#34166=AXIS2_PLACEMENT_3D ( 'NONE', #12535, #33431, #49685 ) ;
#34208=DIRECTION ( 'NONE',  ( -0.000000000000000000, -0.000000000000000000, -1.000000000000000000 ) ) ;
#34230=EDGE_LOOP ( 'NONE', ( #50164, #21480, #5846, #11084 ) ) ;
#34355=CYLINDRICAL_SURFACE ( 'NONE', #26690, 1.000000000000000888 ) ;
#34363=FACE_OUTER_BOUND ( 'NONE', #37813, .T. ) ;
#34372=ADVANCED_FACE ( 'NONE', ( #26847 ), #42748, .F. ) ;
#34442=FACE_OUTER_BOUND ( 'NONE', #4533, .T. ) ;
#34451=CIRCLE ( 'NONE', #42412, 0.7499999999999997780 ) ;
#34501=VECTOR ( 'NONE', #30780, 1000.000000000000000 ) ;
#34513=CARTESIAN_POINT ( 'NONE',  ( 11.19000000000000128, -12.00000000000000000, -4.250000000000000000 ) ) ;
#34536=DIRECTION ( 'NONE',  ( 0.000000000000000000, 0.000000000000000000, 1.000000000000000000 ) ) ;
#34562=ORIENTED_EDGE ( 'NONE', *, *, #60157, .T. ) ;
#34676=VERTEX_POINT ( 'NONE', #60703 ) ;
#34691=AXIS2_PLACEMENT_3D ( 'NONE', #29770, #28127, #17163 ) ;
#34698=PRODUCT_DEFINITION_FORMATION_WITH_SPECIFIED_SOURCE ( 'ANY', '', #17722, .NOT_KNOWN. ) ;
#34699=CARTESIAN_POINT ( 'NONE',  ( 9.249999999999998224, -7.848062532927998269, -5.000000000000000000 ) ) ;
#34737=VERTEX_POINT ( 'NONE', #14366 ) ;
#34740=ORIENTED_EDGE ( 'NONE', *, *, #12248, .F. ) ;
#34824=EDGE_CURVE ( 'NONE', #38359, #47718, #57135, .T. ) ;
#34933=DIRECTION ( 'NONE',  ( 0.000000000000000000, 0.000000000000000000, -1.000000000000000000 ) ) ;
#34960=ORIENTED_EDGE ( 'NONE', *, *, #4726, .F. ) ;
#34967=EDGE_CURVE ( 'NONE', #35206, #7633, #8568, .T. ) ;
#35053=CIRCLE ( 'NONE', #10248, 0.8099999999999999423 ) ;
#35150=CLOSED_SHELL ( 'NONE', ( #41873, #46296, #34372, #41789, #66577, #48171, #17499, #65356, #41844, #62627, #29065, #9382, #44401, #29788, #25765, #10126, #6002, #27377, #23222, #47680, #35865, #68392, #21179, #28187, #43638, #30096, #45418, #62892, #20108, #32842, #19812 ) ) ;
#35154=AXIS2_PLACEMENT_3D ( 'NONE', #8223, #66239, #24147 ) ;
#35177=ORIENTED_EDGE ( 'NONE', *, *, #23811, .T. ) ;
#35206=VERTEX_POINT ( 'NONE', #7908 ) ;
#35219=CARTESIAN_POINT ( 'NONE',  ( -7.281754163448141526, 8.000000000000000000, -1.000000000000000000 ) ) ;
#35426=CARTESIAN_POINT ( 'NONE',  ( 9.249999999999998224, -7.848062532927998269, 0.000000000000000000 ) ) ;
#35441=VERTEX_POINT ( 'NONE', #17663 ) ;
#35496=CARTESIAN_POINT ( 'NONE',  ( 8.249999999999996447, 8.250000000000001776, 0.000000000000000000 ) ) ;
#35570=DIRECTION ( 'NONE',  ( 0.000000000000000000, 0.000000000000000000, 1.000000000000000000 ) ) ;
#35778=CARTESIAN_POINT ( 'NONE',  ( 12.00000000000000178, -11.18999999999999950, 0.000000000000000000 ) ) ;
#35829=CIRCLE ( 'NONE', #61764, 0.8099999999999999423 ) ;
#35865=ADVANCED_FACE ( 'NONE', ( #17222 ), #65018, .T. ) ;
#35888=CYLINDRICAL_SURFACE ( 'NONE', #28242, 1.000000000000000888 ) ;
#35891=APPLICATION_CONTEXT ( 'automotive_design' ) ;
#35895=CARTESIAN_POINT ( 'NONE',  ( -11.18999999999999950, 11.18999999999999950, -4.250000000000000000 ) ) ;
#35912=EDGE_CURVE ( 'NONE', #1047, #59678, #54379, .T. ) ;
#35991=CYLINDRICAL_SURFACE ( 'NONE', #721, 0.7500000000000006661 ) ;
#36083=VECTOR ( 'NONE', #35570, 1000.000000000000000 ) ;
#36087=ORIENTED_EDGE ( 'NONE', *, *, #57659, .F. ) ;
#36118=AXIS2_PLACEMENT_3D ( 'NONE', #32443, #43378, #33471 ) ;
#36139=DIRECTION ( 'NONE',  ( 1.000000000000000000, 0.000000000000000000, 0.000000000000000000 ) ) ;
#36227=CYLINDRICAL_SURFACE ( 'NONE', #61031, 1.000000000000001776 ) ;
#36266=ORIENTED_EDGE ( 'NONE', *, *, #16106, .F. ) ;
#36312=CARTESIAN_POINT ( 'NONE',  ( -8.249999999999996447, -7.848062532927998269, -1.000000000000000000 ) ) ;
#36339=ORIENTED_EDGE ( 'NONE', *, *, #41605, .F. ) ;
#36500=VERTEX_POINT ( 'NONE', #30903 ) ;
#36527=DIRECTION ( 'NONE',  ( 0.000000000000000000, 0.000000000000000000, 1.000000000000000000 ) ) ;
#36631=ORIENTED_EDGE ( 'NONE', *, *, #58058, .F. ) ;
#36702=CIRCLE ( 'NONE', #45710, 0.06000000000000102474 ) ;
#36731=EDGE_LOOP ( 'NONE', ( #16652, #8382, #54470, #21113 ) ) ;
#36779=AXIS2_PLACEMENT_3D ( 'NONE', #38902, #53, #26923 ) ;
#36842=ADVANCED_BREP_SHAPE_REPRESENTATION ( '', ( #65930, #45918 ), #25755 ) ;
#36872=DIRECTION ( 'NONE',  ( 0.000000000000000000, 0.000000000000000000, 1.000000000000000000 ) ) ;
#36993=CARTESIAN_POINT ( 'NONE',  ( 12.00000000000000000, 11.18999999999999950, 0.000000000000000000 ) ) ;
#37037=SURFACE_STYLE_USAGE ( .BOTH. , #21799 ) ;
#37173=AXIS2_PLACEMENT_3D ( 'NONE', #23588, #8016, #45151 ) ;
#37213=FACE_OUTER_BOUND ( 'NONE', #11315, .T. ) ;
#37232=VERTEX_POINT ( 'NONE', #35219 ) ;
#37291=DIRECTION ( 'NONE',  ( -1.000000000000000000, 7.751221965937476285E-17, 0.000000000000000000 ) ) ;
#37296=CIRCLE ( 'NONE', #41768, 1.000000000000000888 ) ;
#37316=CIRCLE ( 'NONE', #3381, 0.7499999999999997780 ) ;
#37375=( NAMED_UNIT ( * ) PLANE_ANGLE_UNIT ( ) SI_UNIT ( $, .RADIAN. ) );
#37409=PRODUCT_CONTEXT ( 'NONE', #52631, 'mechanical' ) ;
#37436=DIRECTION ( 'NONE',  ( -0.000000000000000000, -0.000000000000000000, -1.000000000000000000 ) ) ;
#37465=DIRECTION ( 'NONE',  ( -0.000000000000000000, 0.000000000000000000, -1.000000000000000000 ) ) ;
#37651=DIRECTION ( 'NONE',  ( 0.000000000000000000, 0.000000000000000000, 1.000000000000000000 ) ) ;
#37799=LINE ( 'NONE', #1017, #67055 ) ;
#37813=EDGE_LOOP ( 'NONE', ( #13647, #10076, #11330, #67573 ) ) ;
#37939=EDGE_CURVE ( 'NONE', #11801, #36500, #17421, .T. ) ;
#38120=AXIS2_PLACEMENT_3D ( 'NONE', #58854, #157, #10411 ) ;
#38210=DIRECTION ( 'NONE',  ( 0.000000000000000000, 0.000000000000000000, 1.000000000000000000 ) ) ;
#38275=ORIENTED_EDGE ( 'NONE', *, *, #55539, .F. ) ;
#38311=ORIENTED_EDGE ( 'NONE', *, *, #8105, .T. ) ;
#38359=VERTEX_POINT ( 'NONE', #61461 ) ;
#38376=DIRECTION ( 'NONE',  ( 0.000000000000000000, 0.000000000000000000, 1.000000000000000000 ) ) ;
#38396=PLANE ( 'NONE',  #28766 ) ;
#38490=CARTESIAN_POINT ( 'NONE',  ( -8.000000000000000000, 7.281754163448145079, 0.000000000000000000 ) ) ;
#38543=DIRECTION ( 'NONE',  ( 0.000000000000000000, 0.000000000000000000, 1.000000000000000000 ) ) ;
#38663=CIRCLE ( 'NONE', #63510, 1.000000000000000888 ) ;
#38790=CYLINDRICAL_SURFACE ( 'NONE', #59600, 0.8099999999999999423 ) ;
#38800=ORIENTED_EDGE ( 'NONE', *, *, #44269, .T. ) ;
#38902=CARTESIAN_POINT ( 'NONE',  ( -8.000000000000000000, -8.000000000000000000, -1.000000000000000000 ) ) ;
#38962=VERTEX_POINT ( 'NONE', #15699 ) ;
#39134=EDGE_CURVE ( 'NONE', #1047, #37232, #1171, .T. ) ;
#39431=EDGE_CURVE ( 'NONE', #26669, #15112, #42119, .T. ) ;
#39441=ORIENTED_EDGE ( 'NONE', *, *, #47675, .F. ) ;
#39518=EDGE_LOOP ( 'NONE', ( #69275, #45919, #35177, #24943 ) ) ;
#39653=ORIENTED_EDGE ( 'NONE', *, *, #31168, .F. ) ;
#39771=CARTESIAN_POINT ( 'NONE',  ( -8.249999999999996447, 8.250000000000001776, 5.000000000000000000 ) ) ;
#39840=CARTESIAN_POINT ( 'NONE',  ( -11.25000000000000178, -11.18999999999999950, -5.000000000000000000 ) ) ;
#39873=ORIENTED_EDGE ( 'NONE', *, *, #6126, .F. ) ;
#39947=CIRCLE ( 'NONE', #16258, 1.000000000000000888 ) ;
#39997=EDGE_CURVE ( 'NONE', #48626, #62359, #44116, .T. ) ;
#40180=AXIS2_PLACEMENT_3D ( 'NONE', #56724, #13236, #40813 ) ;
#40229=EDGE_CURVE ( 'NONE', #9548, #41002, #69869, .T. ) ;
#40308=CARTESIAN_POINT ( 'NONE',  ( -11.25000000000000000, 11.18999999999999950, -5.000000000000000000 ) ) ;
#40366=ORIENTED_EDGE ( 'NONE', *, *, #17366, .F. ) ;
#40376=CARTESIAN_POINT ( 'NONE',  ( -7.281754163448141526, 8.000000000000000000, 0.000000000000000000 ) ) ;
#40479=LINE ( 'NONE', #45079, #32151 ) ;
#40488=LINE ( 'NONE', #40840, #28237 ) ;
#40505=DIRECTION ( 'NONE',  ( 1.000000000000000000, 0.000000000000000000, 0.000000000000000000 ) ) ;
#40523=ORIENTED_EDGE ( 'NONE', *, *, #41343, .F. ) ;
#40534=ORIENTED_EDGE ( 'NONE', *, *, #41605, .T. ) ;
#40547=CARTESIAN_POINT ( 'NONE',  ( 11.25000000000000178, -11.18999999999999950, -4.250000000000000000 ) ) ;
#40689=ORIENTED_EDGE ( 'NONE', *, *, #37939, .T. ) ;
#40697=CYLINDRICAL_SURFACE ( 'NONE', #46737, 0.8099999999999999423 ) ;
#40813=DIRECTION ( 'NONE',  ( -1.000000000000000000, 0.000000000000000000, 0.000000000000000000 ) ) ;
#40840=CARTESIAN_POINT ( 'NONE',  ( 12.00000000000000178, -11.18999999999999950, -5.000000000000000000 ) ) ;
#40950=DIRECTION ( 'NONE',  ( -0.000000000000000000, 0.000000000000000000, 1.000000000000000000 ) ) ;
#41002=VERTEX_POINT ( 'NONE', #48410 ) ;
#41166=AXIS2_PLACEMENT_3D ( 'NONE', #41883, #68058, #14664 ) ;
#41257=ORIENTED_EDGE ( 'NONE', *, *, #47675, .T. ) ;
#41300=CARTESIAN_POINT ( 'NONE',  ( -11.18999999999999950, 11.25000000000000178, -4.250000000000000000 ) ) ;
#41343=EDGE_CURVE ( 'NONE', #51919, #4444, #13340, .T. ) ;
#41394=AXIS2_PLACEMENT_3D ( 'NONE', #31180, #3948, #10635 ) ;
#41411=ORIENTED_EDGE ( 'NONE', *, *, #61636, .F. ) ;
#41448=EDGE_CURVE ( 'NONE', #62359, #51203, #27260, .T. ) ;
#41488=ORIENTED_EDGE ( 'NONE', *, *, #61767, .F. ) ;
#41540=FACE_OUTER_BOUND ( 'NONE', #9101, .T. ) ;
#41541=CARTESIAN_POINT ( 'NONE',  ( -12.00000000000000000, 11.18999999999999950, -5.000000000000000000 ) ) ;
#41605=EDGE_CURVE ( 'NONE', #21803, #34676, #65954, .T. ) ;
#41768=AXIS2_PLACEMENT_3D ( 'NONE', #10078, #69825, #53229 ) ;
#41789=ADVANCED_FACE ( 'NONE', ( #14325 ), #35888, .F. ) ;
#41802=CARTESIAN_POINT ( 'NONE',  ( -11.18999999999999950, -11.18999999999999950, -4.250000000000000000 ) ) ;
#41810=CIRCLE ( 'NONE', #19245, 1.000000000000001776 ) ;
#41844=ADVANCED_FACE ( 'NONE', ( #4427 ), #9362, .T. ) ;
#41873=ADVANCED_FACE ( 'NONE', ( #53219 ), #36227, .F. ) ;
#41882=ORIENTED_EDGE ( 'NONE', *, *, #34824, .T. ) ;
#41883=CARTESIAN_POINT ( 'NONE',  ( -11.19000000000000128, -12.00000000000000000, -5.000000000000000000 ) ) ;
#41884=DIRECTION ( 'NONE',  ( -1.000000000000000000, 0.000000000000000000, 0.000000000000000000 ) ) ;
#41967=DIRECTION ( 'NONE',  ( 0.000000000000000000, 0.000000000000000000, -1.000000000000000000 ) ) ;
#41989=EDGE_LOOP ( 'NONE', ( #6000, #40689, #3966, #4242, #51364, #56159 ) ) ;
#41997=CARTESIAN_POINT ( 'NONE',  ( 11.25000000000000000, 11.18999999999999950, -4.250000000000000000 ) ) ;
#42083=CARTESIAN_POINT ( 'NONE',  ( 11.18999999999999950, 12.00000000000000178, 0.000000000000000000 ) ) ;
#42119=LINE ( 'NONE', #68998, #60894 ) ;
#42383=ORIENTED_EDGE ( 'NONE', *, *, #24909, .F. ) ;
#42412=AXIS2_PLACEMENT_3D ( 'NONE', #2297, #44716, #23859 ) ;
#42435=DIRECTION ( 'NONE',  ( 0.000000000000000000, 0.000000000000000000, -1.000000000000000000 ) ) ;
#42446=AXIS2_PLACEMENT_3D ( 'NONE', #112, #49577, #48896 ) ;
#42495=LINE ( 'NONE', #64088, #24012 ) ;
#42623=ORIENTED_EDGE ( 'NONE', *, *, #12994, .T. ) ;
#42748=CYLINDRICAL_SURFACE ( 'NONE', #16418, 1.000000000000000888 ) ;
#42786=AXIS2_PLACEMENT_3D ( 'NONE', #27739, #10435, #11125 ) ;
#42861=CARTESIAN_POINT ( 'NONE',  ( 8.000000000000001776, -6.879816696376140683, -1.000000000000000000 ) ) ;
#42867=ORIENTED_EDGE ( 'NONE', *, *, #37939, .F. ) ;
#42877=DIRECTION ( 'NONE',  ( 0.000000000000000000, 0.000000000000000000, 1.000000000000000000 ) ) ;
#42972=CARTESIAN_POINT ( 'NONE',  ( -11.18999999999999950, -11.25000000000000000, -4.250000000000000000 ) ) ;
#43017=AXIS2_PLACEMENT_3D ( 'NONE', #28859, #50089, #34160 ) ;
#43216=EDGE_LOOP ( 'NONE', ( #68033, #32118, #49532, #54511, #23654, #6498, #23722, #24007, #5569, #1945 ) ) ;
#43259=MECHANICAL_DESIGN_GEOMETRIC_PRESENTATION_REPRESENTATION('',(#68089),#12744);
#43285=AXIS2_PLACEMENT_3D ( 'NONE', #33984, #19383, #40950 ) ;
#43330=CARTESIAN_POINT ( 'NONE',  ( 9.249999999999998224, 8.250000000000001776, 5.000000000000000000 ) ) ;
#43378=DIRECTION ( 'NONE',  ( 7.751221965937476285E-17, 1.000000000000000000, -0.000000000000000000 ) ) ;
#43441=CARTESIAN_POINT ( 'NONE',  ( 12.00000000000000000, 11.18999999999999950, -4.250000000000000000 ) ) ;
#43561=LINE ( 'NONE', #17375, #19459 ) ;
#43565=VERTEX_POINT ( 'NONE', #46723 ) ;
#43607=EDGE_CURVE ( 'NONE', #54089, #60836, #66124, .T. ) ;
#43638=ADVANCED_FACE ( 'NONE', ( #59089 ), #5367, .F. ) ;
#43694=FACE_BOUND ( 'NONE', #26677, .T. ) ;
#43766=DIRECTION ( 'NONE',  ( 0.000000000000000000, 0.000000000000000000, 1.000000000000000000 ) ) ;
#43888=DIRECTION ( 'NONE',  ( 7.751221965937476285E-17, -1.000000000000000000, -0.000000000000000000 ) ) ;
#43963=ORIENTED_EDGE ( 'NONE', *, *, #66614, .F. ) ;
#44012=EDGE_CURVE ( 'NONE', #15758, #52731, #60032, .T. ) ;
#44116=LINE ( 'NONE', #49083, #62097 ) ;
#44152=CIRCLE ( 'NONE', #35154, 1.000000000000001776 ) ;
#44185=ORIENTED_EDGE ( 'NONE', *, *, #5982, .F. ) ;
#44269=EDGE_CURVE ( 'NONE', #11693, #4189, #33327, .T. ) ;
#44339=CARTESIAN_POINT ( 'NONE',  ( -11.25000000000000000, 11.18999999999999950, -4.250000000000000000 ) ) ;
#44361=FACE_BOUND ( 'NONE', #32627, .T. ) ;
#44383=CARTESIAN_POINT ( 'NONE',  ( 11.18999999999999950, -11.18999999999999950, 0.000000000000000000 ) ) ;
#44401=ADVANCED_FACE ( 'NONE', ( #10135 ), #38396, .T. ) ;
#44463=EDGE_CURVE ( 'NONE', #52731, #48724, #34451, .T. ) ;
#44479=CARTESIAN_POINT ( 'NONE',  ( -11.18999999999999950, 11.18999999999999950, -5.000000000000000000 ) ) ;
#44558=ORIENTED_EDGE ( 'NONE', *, *, #23811, .F. ) ;
#44640=ORIENTED_EDGE ( 'NONE', *, *, #44463, .T. ) ;
#44716=DIRECTION ( 'NONE',  ( 1.000000000000000000, -0.000000000000000000, 0.000000000000000000 ) ) ;
#44742=DIRECTION ( 'NONE',  ( 0.000000000000000000, -1.000000000000000000, 0.000000000000000000 ) ) ;
#44744=EDGE_CURVE ( 'NONE', #17547, #64954, #48933, .T. ) ;
#44840=VECTOR ( 'NONE', #38376, 1000.000000000000000 ) ;
#44851=ORIENTED_EDGE ( 'NONE', *, *, #40229, .T. ) ;
#44924=LINE ( 'NONE', #55881, #26860 ) ;
#44978=CARTESIAN_POINT ( 'NONE',  ( 8.000000000000000000, 8.000000000000001776, -1.000000000000000000 ) ) ;
#45079=CARTESIAN_POINT ( 'NONE',  ( -8.000000000000000000, -8.000000000000000000, -1.000000000000000000 ) ) ;
#45151=DIRECTION ( 'NONE',  ( 1.000000000000000000, 0.000000000000000000, 0.000000000000000000 ) ) ;
#45221=EDGE_LOOP ( 'NONE', ( #14446, #30600, #41882, #16398, #30219, #7045, #14693, #11071 ) ) ;
#45325=DIRECTION ( 'NONE',  ( -0.000000000000000000, -1.000000000000000000, -0.000000000000000000 ) ) ;
#45375=ORIENTED_EDGE ( 'NONE', *, *, #50578, .T. ) ;
#45396=PLANE ( 'NONE',  #100 ) ;
#45418=ADVANCED_FACE ( 'NONE', ( #12858 ), #24189, .T. ) ;
#45426=CARTESIAN_POINT ( 'NONE',  ( 8.000000000000000000, 8.000000000000001776, 0.000000000000000000 ) ) ;
#45450=DIRECTION ( 'NONE',  ( -0.000000000000000000, 0.000000000000000000, -1.000000000000000000 ) ) ;
#45710=AXIS2_PLACEMENT_3D ( 'NONE', #44479, #34208, #51187 ) ;
#45742=DIRECTION ( 'NONE',  ( 1.000000000000000000, 0.000000000000000000, -0.000000000000000000 ) ) ;
#45750=EDGE_CURVE ( 'NONE', #52724, #19489, #1870, .T. ) ;
#45860=FACE_OUTER_BOUND ( 'NONE', #25102, .T. ) ;
#45914=CIRCLE ( 'NONE', #49324, 1.000000000000001776 ) ;
#45918=AXIS2_PLACEMENT_3D ( 'NONE', #22775, #53934, #32355 ) ;
#45919=ORIENTED_EDGE ( 'NONE', *, *, #39431, .T. ) ;
#45995=ORIENTED_EDGE ( 'NONE', *, *, #65586, .T. ) ;
#46110=DIRECTION ( 'NONE',  ( -1.084202172485504434E-16, 1.000000000000000000, 0.000000000000000000 ) ) ;
#46136=CARTESIAN_POINT ( 'NONE',  ( 7.249999999999995559, 8.250000000000001776, 0.000000000000000000 ) ) ;
#46251=ORIENTED_EDGE ( 'NONE', *, *, #12982, .T. ) ;
#46296=ADVANCED_FACE ( 'NONE', ( #51952 ), #31790, .F. ) ;
#46345=TOROIDAL_SURFACE ( 'NONE', #5741, 0.06000000000000080963, 0.7500000000000000000 ) ;
#46388=CARTESIAN_POINT ( 'NONE',  ( 8.000000000000000000, 8.000000000000001776, -1.000000000000000000 ) ) ;
#46602=ORIENTED_EDGE ( 'NONE', *, *, #694, .T. ) ;
#46694=EDGE_CURVE ( 'NONE', #56088, #56996, #51864, .T. ) ;
#46723=CARTESIAN_POINT ( 'NONE',  ( 11.19000000000000128, -12.00000000000000000, 0.000000000000000000 ) ) ;
#46737=AXIS2_PLACEMENT_3D ( 'NONE', #56950, #4294, #47403 ) ;
#46781=VERTEX_POINT ( 'NONE', #54656 ) ;
#47027=EDGE_CURVE ( 'NONE', #21803, #63045, #26925, .T. ) ;
#47127=DIRECTION ( 'NONE',  ( -1.000000000000000000, 0.000000000000000000, 0.000000000000000000 ) ) ;
#47212=DIRECTION ( 'NONE',  ( 1.000000000000000000, 0.000000000000000000, 0.000000000000000000 ) ) ;
#47282=EDGE_CURVE ( 'NONE', #15112, #56088, #66466, .T. ) ;
#47333=ORIENTED_EDGE ( 'NONE', *, *, #54030, .T. ) ;
#47403=DIRECTION ( 'NONE',  ( 1.000000000000000000, 0.000000000000000000, 0.000000000000000000 ) ) ;
#47433=DIRECTION ( 'NONE',  ( 1.000000000000000000, 0.000000000000000000, 0.000000000000000000 ) ) ;
#47590=CIRCLE ( 'NONE', #19359, 0.8099999999999999423 ) ;
#47605=DIRECTION ( 'NONE',  ( 7.751221965937476285E-17, 1.000000000000000000, -0.000000000000000000 ) ) ;
#47631=ORIENTED_EDGE ( 'NONE', *, *, #31168, .T. ) ;
#47632=DIRECTION ( 'NONE',  ( 0.000000000000000000, 0.000000000000000000, 1.000000000000000000 ) ) ;
#47675=EDGE_CURVE ( 'NONE', #57047, #48724, #29248, .T. ) ;
#47680=ADVANCED_FACE ( 'NONE', ( #45860 ), #4414, .T. ) ;
#47718=VERTEX_POINT ( 'NONE', #24652 ) ;
#47737=LINE ( 'NONE', #31493, #34501 ) ;
#47751=CARTESIAN_POINT ( 'NONE',  ( -8.249999999999996447, -7.848062532927998269, 0.000000000000000000 ) ) ;
#47813=CARTESIAN_POINT ( 'NONE',  ( -11.18999999999999950, 12.00000000000000178, -4.250000000000000000 ) ) ;
#47884=DIRECTION ( 'NONE',  ( -0.000000000000000000, -0.000000000000000000, -1.000000000000000000 ) ) ;
#47909=CARTESIAN_POINT ( 'NONE',  ( 9.249999999999998224, 8.250000000000001776, -5.000000000000000000 ) ) ;
#47977=FILL_AREA_STYLE ('',( #26413 ) ) ;
#47989=VECTOR ( 'NONE', #19609, 1000.000000000000000 ) ;
#48038=CARTESIAN_POINT ( 'NONE',  ( 8.249999999999996447, -7.848062532927998269, 5.000000000000000000 ) ) ;
#48086=ORIENTED_EDGE ( 'NONE', *, *, #44744, .F. ) ;
#48167=DIRECTION ( 'NONE',  ( 1.000000000000000000, 0.000000000000000000, -0.000000000000000000 ) ) ;
#48171=ADVANCED_FACE ( 'NONE', ( #2300 ), #8286, .T. ) ;
#48344=ORIENTED_EDGE ( 'NONE', *, *, #55883, .T. ) ;
#48407=CARTESIAN_POINT ( 'NONE',  ( -8.249999999999996447, -7.848062532927998269, 5.000000000000000000 ) ) ;
#48410=CARTESIAN_POINT ( 'NONE',  ( -8.000000000000000000, -6.879816696376141572, -1.000000000000000000 ) ) ;
#48500=VECTOR ( 'NONE', #47632, 1000.000000000000000 ) ;
#48602=LINE ( 'NONE', #16081, #12684 ) ;
#48626=VERTEX_POINT ( 'NONE', #35426 ) ;
#48724=VERTEX_POINT ( 'NONE', #14933 ) ;
#48764=EDGE_LOOP ( 'NONE', ( #50727, #55469, #33304, #6646 ) ) ;
#48800=CARTESIAN_POINT ( 'NONE',  ( 7.281754163448140638, 8.000000000000001776, 0.000000000000000000 ) ) ;
#48896=DIRECTION ( 'NONE',  ( 1.000000000000000000, 0.000000000000000000, 0.000000000000000000 ) ) ;
#48933=LINE ( 'NONE', #31289, #66062 ) ;
#49027=DIRECTION ( 'NONE',  ( 0.000000000000000000, 0.000000000000000000, 1.000000000000000000 ) ) ;
#49083=CARTESIAN_POINT ( 'NONE',  ( 9.249999999999998224, -7.848062532927998269, 5.000000000000000000 ) ) ;
#49105=AXIS2_PLACEMENT_3D ( 'NONE', #41300, #68176, #34933 ) ;
#49123=DIRECTION ( 'NONE',  ( 0.000000000000000000, 0.000000000000000000, 1.000000000000000000 ) ) ;
#49163=VERTEX_POINT ( 'NONE', #6957 ) ;
#49285=EDGE_CURVE ( 'NONE', #14752, #5450, #3409, .T. ) ;
#49290=CARTESIAN_POINT ( 'NONE',  ( -8.249999999999996447, -7.848062532927998269, -1.000000000000000000 ) ) ;
#49320=CARTESIAN_POINT ( 'NONE',  ( -11.18999999999999950, 11.18999999999999950, 0.000000000000000000 ) ) ;
#49324=AXIS2_PLACEMENT_3D ( 'NONE', #36312, #29243, #9094 ) ;
#49445=CARTESIAN_POINT ( 'NONE',  ( 7.249999999999995559, -7.848062532927998269, 5.000000000000000000 ) ) ;
#49532=ORIENTED_EDGE ( 'NONE', *, *, #8481, .F. ) ;
#49561=ORIENTED_EDGE ( 'NONE', *, *, #10170, .T. ) ;
#49569=AXIS2_PLACEMENT_3D ( 'NONE', #18991, #24295, #12620 ) ;
#49577=DIRECTION ( 'NONE',  ( 0.000000000000000000, 0.000000000000000000, 1.000000000000000000 ) ) ;
#49685=DIRECTION ( 'NONE',  ( 1.000000000000000000, 0.000000000000000000, -0.000000000000000000 ) ) ;
#49742=CARTESIAN_POINT ( 'NONE',  ( -8.000000000000000000, 7.281754163448145079, 5.000000000000000000 ) ) ;
#49755=DIRECTION ( 'NONE',  ( 0.000000000000000000, -1.000000000000000000, 0.000000000000000000 ) ) ;
#50089=DIRECTION ( 'NONE',  ( 0.000000000000000000, 0.000000000000000000, -1.000000000000000000 ) ) ;
#50114=CARTESIAN_POINT ( 'NONE',  ( -11.18999999999999950, 11.25000000000000178, -5.000000000000000000 ) ) ;
#50164=ORIENTED_EDGE ( 'NONE', *, *, #8105, .F. ) ;
#50281=CARTESIAN_POINT ( 'NONE',  ( 11.19000000000000128, -12.00000000000000000, -4.250000000000000000 ) ) ;
#50413=CARTESIAN_POINT ( 'NONE',  ( 8.000000000000001776, -6.879816696376140683, 0.000000000000000000 ) ) ;
#50508=DIRECTION ( 'NONE',  ( -1.000000000000000000, 0.000000000000000000, 0.000000000000000000 ) ) ;
#50565=VECTOR ( 'NONE', #28623, 1000.000000000000000 ) ;
#50578=EDGE_CURVE ( 'NONE', #43565, #16217, #35053, .T. ) ;
#50727=ORIENTED_EDGE ( 'NONE', *, *, #49285, .F. ) ;
#50943=ORIENTED_EDGE ( 'NONE', *, *, #24909, .T. ) ;
#50964=CYLINDRICAL_SURFACE ( 'NONE', #68440, 0.7499999999999997780 ) ;
#50990=CARTESIAN_POINT ( 'NONE',  ( -11.25000000000000178, -11.18999999999999950, -4.250000000000000000 ) ) ;
#51073=CARTESIAN_POINT ( 'NONE',  ( 8.249999999999996447, 8.250000000000001776, -1.000000000000000000 ) ) ;
#51132=DIRECTION ( 'NONE',  ( 1.000000000000000000, 0.000000000000000000, -0.000000000000000000 ) ) ;
#51187=DIRECTION ( 'NONE',  ( 1.000000000000000000, 0.000000000000000000, 0.000000000000000000 ) ) ;
#51203=VERTEX_POINT ( 'NONE', #63734 ) ;
#51214=ORIENTED_EDGE ( 'NONE', *, *, #25900, .T. ) ;
#51255=DIRECTION ( 'NONE',  ( -0.000000000000000000, -0.000000000000000000, -1.000000000000000000 ) ) ;
#51327=EDGE_CURVE ( 'NONE', #15112, #35206, #47590, .T. ) ;
#51364=ORIENTED_EDGE ( 'NONE', *, *, #60831, .T. ) ;
#51383=AXIS2_PLACEMENT_3D ( 'NONE', #40547, #8364, #20041 ) ;
#51522=AXIS2_PLACEMENT_3D ( 'NONE', #47751, #38543, #53421 ) ;
#51542=AXIS2_PLACEMENT_3D ( 'NONE', #7912, #29488, #45742 ) ;
#51561=FACE_OUTER_BOUND ( 'NONE', #68290, .T. ) ;
#51711=PLANE ( 'NONE',  #23442 ) ;
#51817=EDGE_CURVE ( 'NONE', #34737, #57047, #67977, .T. ) ;
#51864=LINE ( 'NONE', #26049, #29075 ) ;
#51919=VERTEX_POINT ( 'NONE', #3374 ) ;
#51952=FACE_OUTER_BOUND ( 'NONE', #29140, .T. ) ;
#52030=ORIENTED_EDGE ( 'NONE', *, *, #45750, .T. ) ;
#52114=ORIENTED_EDGE ( 'NONE', *, *, #31150, .F. ) ;
#52324=AXIS2_PLACEMENT_3D ( 'NONE', #51073, #58417, #47433 ) ;
#52395=DIRECTION ( 'NONE',  ( 1.000000000000000000, 0.000000000000000000, 0.000000000000000000 ) ) ;
#52401=CIRCLE ( 'NONE', #61392, 1.000000000000001776 ) ;
#52499=LINE ( 'NONE', #4069, #18369 ) ;
#52631=APPLICATION_CONTEXT ( 'automotive_design' ) ;
#52724=VERTEX_POINT ( 'NONE', #42861 ) ;
#52731=VERTEX_POINT ( 'NONE', #54187 ) ;
#52808=EDGE_LOOP ( 'NONE', ( #28169, #41257, #21136, #6197 ) ) ;
#52858=DIRECTION ( 'NONE',  ( -0.000000000000000000, -0.000000000000000000, -1.000000000000000000 ) ) ;
#52939=DIRECTION ( 'NONE',  ( 1.000000000000000000, 7.751221965937476285E-17, -0.000000000000000000 ) ) ;
#53008=VERTEX_POINT ( 'NONE', #42083 ) ;
#53147=DIRECTION ( 'NONE',  ( 1.000000000000000000, 0.000000000000000000, 0.000000000000000000 ) ) ;
#53219=FACE_OUTER_BOUND ( 'NONE', #9920, .T. ) ;
#53229=DIRECTION ( 'NONE',  ( 1.000000000000000000, 0.000000000000000000, 0.000000000000000000 ) ) ;
#53421=DIRECTION ( 'NONE',  ( 1.000000000000000000, 0.000000000000000000, 0.000000000000000000 ) ) ;
#53551=FACE_OUTER_BOUND ( 'NONE', #13746, .T. ) ;
#53599=LINE ( 'NONE', #36993, #66308 ) ;
#53711=VECTOR ( 'NONE', #1010, 1000.000000000000000 ) ;
#53716=LINE ( 'NONE', #69273, #25092 ) ;
#53719=DIRECTION ( 'NONE',  ( -0.000000000000000000, -0.000000000000000000, -1.000000000000000000 ) ) ;
#53729=DIRECTION ( 'NONE',  ( 1.000000000000000000, 0.000000000000000000, 0.000000000000000000 ) ) ;
#53778=AXIS2_PLACEMENT_3D ( 'NONE', #57139, #56433, #62078 ) ;
#53934=DIRECTION ( 'NONE',  ( 0.000000000000000000, 0.000000000000000000, 1.000000000000000000 ) ) ;
#53942=VERTEX_POINT ( 'NONE', #50281 ) ;
#54030=EDGE_CURVE ( 'NONE', #7633, #56088, #11307, .T. ) ;
#54071=ORIENTED_EDGE ( 'NONE', *, *, #14255, .T. ) ;
#54089=VERTEX_POINT ( 'NONE', #40376 ) ;
#54187=CARTESIAN_POINT ( 'NONE',  ( 11.18999999999999950, 11.25000000000000178, -5.000000000000000000 ) ) ;
#54343=CARTESIAN_POINT ( 'NONE',  ( 11.25000000000000178, 11.18999999999999950, -4.250000000000000000 ) ) ;
#54378=DIRECTION ( 'NONE',  ( 1.000000000000000000, 0.000000000000000000, 0.000000000000000000 ) ) ;
#54379=LINE ( 'NONE', #22199, #64034 ) ;
#54470=ORIENTED_EDGE ( 'NONE', *, *, #34967, .F. ) ;
#54482=CARTESIAN_POINT ( 'NONE',  ( -11.19000000000000128, -12.00000000000000000, -5.000000000000000000 ) ) ;
#54511=ORIENTED_EDGE ( 'NONE', *, *, #9387, .T. ) ;
#54570=DIRECTION ( 'NONE',  ( -0.000000000000000000, -0.000000000000000000, -1.000000000000000000 ) ) ;
#54656=CARTESIAN_POINT ( 'NONE',  ( -9.249999999999998224, 8.250000000000001776, 0.000000000000000000 ) ) ;
#54658=CARTESIAN_POINT ( 'NONE',  ( -8.000000000000000000, 8.000000000000000000, 0.000000000000000000 ) ) ;
#54866=ORIENTED_EDGE ( 'NONE', *, *, #60429, .F. ) ;
#55163=LINE ( 'NONE', #54482, #50565 ) ;
#55179=CARTESIAN_POINT ( 'NONE',  ( 11.19000000000000128, -12.00000000000000000, -5.000000000000000000 ) ) ;
#55260=DIRECTION ( 'NONE',  ( -0.000000000000000000, -0.000000000000000000, -1.000000000000000000 ) ) ;
#55333=ORIENTED_EDGE ( 'NONE', *, *, #58802, .T. ) ;
#55469=ORIENTED_EDGE ( 'NONE', *, *, #345, .T. ) ;
#55539=EDGE_CURVE ( 'NONE', #53942, #43565, #69007, .T. ) ;
#55550=PRODUCT_DEFINITION_SHAPE ( 'NONE', 'NONE',  #9788 ) ;
#55622=AXIS2_PLACEMENT_3D ( 'NONE', #13167, #30139, #61593 ) ;
#55628=ORIENTED_EDGE ( 'NONE', *, *, #57121, .F. ) ;
#55658=DIRECTION ( 'NONE',  ( 0.000000000000000000, 1.000000000000000000, 0.000000000000000000 ) ) ;
#55697=LINE ( 'NONE', #65618, #1906 ) ;
#55881=CARTESIAN_POINT ( 'NONE',  ( -12.00000000000000000, -11.18999999999999950, -5.000000000000000000 ) ) ;
#55883=EDGE_CURVE ( 'NONE', #63858, #49163, #53716, .T. ) ;
#56088=VERTEX_POINT ( 'NONE', #39840 ) ;
#56159=ORIENTED_EDGE ( 'NONE', *, *, #61747, .F. ) ;
#56372=AXIS2_PLACEMENT_3D ( 'NONE', #29864, #56388, #23164 ) ;
#56388=DIRECTION ( 'NONE',  ( 0.000000000000000000, 0.000000000000000000, 1.000000000000000000 ) ) ;
#56433=DIRECTION ( 'NONE',  ( 0.000000000000000000, 0.000000000000000000, -1.000000000000000000 ) ) ;
#56482=DIRECTION ( 'NONE',  ( 0.000000000000000000, 0.000000000000000000, 1.000000000000000000 ) ) ;
#56502=AXIS2_PLACEMENT_3D ( 'NONE', #41541, #37291, #69460 ) ;
#56724=CARTESIAN_POINT ( 'NONE',  ( 8.249999999999996447, 8.250000000000001776, 5.000000000000000000 ) ) ;
#56823=CARTESIAN_POINT ( 'NONE',  ( 12.00000000000000000, 11.18999999999999950, 0.000000000000000000 ) ) ;
#56829=ORIENTED_EDGE ( 'NONE', *, *, #44463, .F. ) ;
#56950=CARTESIAN_POINT ( 'NONE',  ( -11.18999999999999950, -11.18999999999999950, -5.000000000000000000 ) ) ;
#56996=VERTEX_POINT ( 'NONE', #40308 ) ;
#57047=VERTEX_POINT ( 'NONE', #43441 ) ;
#57121=EDGE_CURVE ( 'NONE', #36500, #38962, #18448, .T. ) ;
#57135=CIRCLE ( 'NONE', #53778, 1.000000000000000888 ) ;
#57139=CARTESIAN_POINT ( 'NONE',  ( -8.249999999999996447, 8.250000000000001776, -5.000000000000000000 ) ) ;
#57321=ORIENTED_EDGE ( 'NONE', *, *, #66315, .T. ) ;
#57365=DIRECTION ( 'NONE',  ( 0.000000000000000000, 0.000000000000000000, 1.000000000000000000 ) ) ;
#57385=EDGE_CURVE ( 'NONE', #17547, #59678, #38663, .T. ) ;
#57548=ORIENTED_EDGE ( 'NONE', *, *, #61636, .T. ) ;
#57659=EDGE_CURVE ( 'NONE', #48724, #53008, #48602, .T. ) ;
#57725=VECTOR ( 'NONE', #3785, 1000.000000000000000 ) ;
#57821=VERTEX_POINT ( 'NONE', #67294 ) ;
#58042=CIRCLE ( 'NONE', #465, 0.8099999999999999423 ) ;
#58058=EDGE_CURVE ( 'NONE', #48724, #14752, #58447, .T. ) ;
#58230=ORIENTED_EDGE ( 'NONE', *, *, #43607, .F. ) ;
#58279=ORIENTED_EDGE ( 'NONE', *, *, #4726, .T. ) ;
#58417=DIRECTION ( 'NONE',  ( 0.000000000000000000, 0.000000000000000000, 1.000000000000000000 ) ) ;
#58424=ORIENTED_EDGE ( 'NONE', *, *, #47027, .F. ) ;
#58447=LINE ( 'NONE', #47813, #66958 ) ;
#58568=AXIS2_PLACEMENT_3D ( 'NONE', #50990, #45325, #66894 ) ;
#58759=VERTEX_POINT ( 'NONE', #47909 ) ;
#58777=DIRECTION ( 'NONE',  ( 1.000000000000000000, 0.000000000000000000, 0.000000000000000000 ) ) ;
#58802=EDGE_CURVE ( 'NONE', #5450, #63858, #58042, .T. ) ;
#58854=CARTESIAN_POINT ( 'NONE',  ( -11.18999999999999950, 11.25000000000000178, -4.250000000000000000 ) ) ;
#58996=DIRECTION ( 'NONE',  ( -1.000000000000000000, 0.000000000000000000, 0.000000000000000000 ) ) ;
#59003=DIRECTION ( 'NONE',  ( 1.000000000000000000, -0.000000000000000000, -0.000000000000000000 ) ) ;
#59089=FACE_OUTER_BOUND ( 'NONE', #9369, .T. ) ;
#59126=ORIENTED_EDGE ( 'NONE', *, *, #32449, .F. ) ;
#59493=ORIENTED_EDGE ( 'NONE', *, *, #16075, .T. ) ;
#59515=ORIENTED_EDGE ( 'NONE', *, *, #67959, .F. ) ;
#59554=VECTOR ( 'NONE', #15428, 1000.000000000000000 ) ;
#59592=EDGE_CURVE ( 'NONE', #26669, #63858, #19815, .T. ) ;
#59600=AXIS2_PLACEMENT_3D ( 'NONE', #60708, #12252, #54378 ) ;
#59655=CYLINDRICAL_SURFACE ( 'NONE', #36118, 0.7500000000000006661 ) ;
#59678=VERTEX_POINT ( 'NONE', #48800 ) ;
#59829=DIRECTION ( 'NONE',  ( -0.000000000000000000, -0.000000000000000000, -1.000000000000000000 ) ) ;
#59894=EDGE_CURVE ( 'NONE', #15758, #14752, #25384, .T. ) ;
#59912=AXIS2_PLACEMENT_3D ( 'NONE', #10372, #32634, #20270 ) ;
#59913=DIRECTION ( 'NONE',  ( 1.000000000000000000, 0.000000000000000000, 0.000000000000000000 ) ) ;
#60010=LINE ( 'NONE', #283, #7639 ) ;
#60032=LINE ( 'NONE', #304, #25516 ) ;
#60046=EDGE_LOOP ( 'NONE', ( #36087, #60200, #26921, #9223 ) ) ;
#60079=CARTESIAN_POINT ( 'NONE',  ( 11.19000000000000128, -11.25000000000000178, -5.000000000000000000 ) ) ;
#60125=DIRECTION ( 'NONE',  ( 0.000000000000000000, 0.000000000000000000, 1.000000000000000000 ) ) ;
#60157=EDGE_CURVE ( 'NONE', #67890, #30509, #33482, .T. ) ;
#60161=CARTESIAN_POINT ( 'NONE',  ( 7.261609891743268541, -8.000000000000000000, 0.000000000000000000 ) ) ;
#60200=ORIENTED_EDGE ( 'NONE', *, *, #58058, .T. ) ;
#60228=SHAPE_REPRESENTATION ( 'END CAP_6266N13', ( #45918 ), #25755 ) ;
#60392=AXIS2_PLACEMENT_3D ( 'NONE', #15587, #26528, #42435 ) ;
#60429=EDGE_CURVE ( 'NONE', #48626, #18593, #60501, .T. ) ;
#60501=CIRCLE ( 'NONE', #42446, 1.000000000000000888 ) ;
#60703=CARTESIAN_POINT ( 'NONE',  ( 8.000000000000000000, 7.281754163448145079, -1.000000000000000000 ) ) ;
#60708=CARTESIAN_POINT ( 'NONE',  ( 11.18999999999999950, 11.18999999999999950, -5.000000000000000000 ) ) ;
#60831=EDGE_CURVE ( 'NONE', #21103, #51919, #6358, .T. ) ;
#60836=VERTEX_POINT ( 'NONE', #64377 ) ;
#60860=PLANE ( 'NONE',  #43285 ) ;
#60861=EDGE_LOOP ( 'NONE', ( #38275, #31279, #69129, #6893 ) ) ;
#60894=VECTOR ( 'NONE', #10306, 1000.000000000000000 ) ;
#60896=EDGE_CURVE ( 'NONE', #46781, #30509, #7499, .T. ) ;
#60999=CIRCLE ( 'NONE', #59912, 1.000000000000001776 ) ;
#61031=AXIS2_PLACEMENT_3D ( 'NONE', #20319, #47884, #41884 ) ;
#61314=CYLINDRICAL_SURFACE ( 'NONE', #40180, 1.000000000000001776 ) ;
#61319=FACE_BOUND ( 'NONE', #19463, .T. ) ;
#61370=ORIENTED_EDGE ( 'NONE', *, *, #26124, .F. ) ;
#61375=ORIENTED_EDGE ( 'NONE', *, *, #59894, .F. ) ;
#61392=AXIS2_PLACEMENT_3D ( 'NONE', #69375, #30494, #58777 ) ;
#61422=ORIENTED_EDGE ( 'NONE', *, *, #67251, .T. ) ;
#61461=CARTESIAN_POINT ( 'NONE',  ( -7.249999999999995559, 8.250000000000001776, -5.000000000000000000 ) ) ;
#61571=CARTESIAN_POINT ( 'NONE',  ( -11.18999999999999950, -11.18999999999999950, -5.000000000000000000 ) ) ;
#61593=DIRECTION ( 'NONE',  ( 1.000000000000000000, 0.000000000000000000, 0.000000000000000000 ) ) ;
#61636=EDGE_CURVE ( 'NONE', #16217, #22012, #53599, .T. ) ;
#61747=EDGE_CURVE ( 'NONE', #35441, #51919, #5158, .T. ) ;
#61764=AXIS2_PLACEMENT_3D ( 'NONE', #6671, #49123, #50508 ) ;
#61767=EDGE_CURVE ( 'NONE', #51203, #62359, #33546, .T. ) ;
#61768=AXIS2_PLACEMENT_3D ( 'NONE', #6277, #27848, #17568 ) ;
#62004=AXIS2_PLACEMENT_3D ( 'NONE', #31569, #5402, #53147 ) ;
#62078=DIRECTION ( 'NONE',  ( -1.000000000000000000, 0.000000000000000000, 0.000000000000000000 ) ) ;
#62097=VECTOR ( 'NONE', #22223, 1000.000000000000000 ) ;
#62359=VERTEX_POINT ( 'NONE', #34699 ) ;
#62438=CARTESIAN_POINT ( 'NONE',  ( 7.249999999999995559, -7.848062532927998269, -1.000000000000000000 ) ) ;
#62627=ADVANCED_FACE ( 'NONE', ( #376 ), #26551, .T. ) ;
#62636=VERTEX_POINT ( 'NONE', #11316 ) ;
#62650=DIRECTION ( 'NONE',  ( -7.751221965937476285E-17, 1.000000000000000000, 0.000000000000000000 ) ) ;
#62892=ADVANCED_FACE ( 'NONE', ( #31072 ), #20461, .F. ) ;
#62985=AXIS2_PLACEMENT_3D ( 'NONE', #33587, #6380, #66104 ) ;
#63045=VERTEX_POINT ( 'NONE', #63957 ) ;
#63378=CARTESIAN_POINT ( 'NONE',  ( 11.18999999999999950, -11.18999999999999950, 0.000000000000000000 ) ) ;
#63379=DIRECTION ( 'NONE',  ( 1.000000000000000000, 0.000000000000000000, 0.000000000000000000 ) ) ;
#63468=EDGE_CURVE ( 'NONE', #63045, #58759, #555, .T. ) ;
#63503=UNCERTAINTY_MEASURE_WITH_UNIT (LENGTH_MEASURE( 1.000000000000000082E-05 ), #4504, 'distance_accuracy_value', 'NONE');
#63510=AXIS2_PLACEMENT_3D ( 'NONE', #68148, #56482, #3103 ) ;
#63734=CARTESIAN_POINT ( 'NONE',  ( 7.249999999999995559, -7.848062532927998269, -5.000000000000000000 ) ) ;
#63858=VERTEX_POINT ( 'NONE', #20204 ) ;
#63957=CARTESIAN_POINT ( 'NONE',  ( 9.249999999999998224, 8.250000000000001776, 0.000000000000000000 ) ) ;
#64002=ORIENTED_EDGE ( 'NONE', *, *, #61747, .T. ) ;
#64034=VECTOR ( 'NONE', #43766, 1000.000000000000000 ) ;
#64041=DIRECTION ( 'NONE',  ( 1.000000000000000000, 0.000000000000000000, 0.000000000000000000 ) ) ;
#64071=DIRECTION ( 'NONE',  ( 0.000000000000000000, 0.000000000000000000, 1.000000000000000000 ) ) ;
#64074=AXIS2_PLACEMENT_3D ( 'NONE', #65920, #33414, #6867 ) ;
#64088=CARTESIAN_POINT ( 'NONE',  ( 12.00000000000000000, 11.18999999999999950, -4.250000000000000000 ) ) ;
#64259=VECTOR ( 'NONE', #2197, 1000.000000000000000 ) ;
#64377=CARTESIAN_POINT ( 'NONE',  ( -7.249999999999995559, 8.250000000000001776, 0.000000000000000000 ) ) ;
#64556=DIRECTION ( 'NONE',  ( -7.751221965937476285E-17, 1.000000000000000000, -0.000000000000000000 ) ) ;
#64588=( NAMED_UNIT ( * ) SI_UNIT ( $, .STERADIAN. ) SOLID_ANGLE_UNIT ( ) );
#64700=ORIENTED_EDGE ( 'NONE', *, *, #34967, .T. ) ;
#64786=DIRECTION ( 'NONE',  ( -1.000000000000000000, 0.000000000000000000, 0.000000000000000000 ) ) ;
#64954=VERTEX_POINT ( 'NONE', #6894 ) ;
#65018=TOROIDAL_SURFACE ( 'NONE', #61768, 0.06000000000000080963, 0.7500000000000000000 ) ;
#65023=DIRECTION ( 'NONE',  ( -1.000000000000000000, 0.000000000000000000, -0.000000000000000000 ) ) ;
#65076=CARTESIAN_POINT ( 'NONE',  ( -8.249999999999996447, 8.250000000000001776, 0.000000000000000000 ) ) ;
#65159=CARTESIAN_POINT ( 'NONE',  ( -8.249999999999996447, -7.848062532927998269, 0.000000000000000000 ) ) ;
#65201=EDGE_CURVE ( 'NONE', #53008, #5450, #29732, .T. ) ;
#65240=( NAMED_UNIT ( * ) SI_UNIT ( $, .STERADIAN. ) SOLID_ANGLE_UNIT ( ) );
#65299=ORIENTED_EDGE ( 'NONE', *, *, #32046, .F. ) ;
#65356=ADVANCED_FACE ( 'NONE', ( #19827 ), #40697, .T. ) ;
#65412=EDGE_CURVE ( 'NONE', #19489, #57821, #16266, .T. ) ;
#65562=ORIENTED_EDGE ( 'NONE', *, *, #9387, .F. ) ;
#65586=EDGE_CURVE ( 'NONE', #11693, #57047, #42495, .T. ) ;
#65618=CARTESIAN_POINT ( 'NONE',  ( -11.19000000000000128, -12.00000000000000000, 0.000000000000000000 ) ) ;
#65759=DIRECTION ( 'NONE',  ( 1.000000000000000000, 0.000000000000000000, 0.000000000000000000 ) ) ;
#65913=DIRECTION ( 'NONE',  ( 0.000000000000000000, 0.000000000000000000, 1.000000000000000000 ) ) ;
#65920=CARTESIAN_POINT ( 'NONE',  ( 8.249999999999996447, -7.848062532927998269, -5.000000000000000000 ) ) ;
#65930=MANIFOLD_SOLID_BREP ( 'Cut-Extrude5', #35150 ) ;
#65954=LINE ( 'NONE', #17523, #14723 ) ;
#65984=ORIENTED_EDGE ( 'NONE', *, *, #16818, .T. ) ;
#66025=LINE ( 'NONE', #49445, #53711 ) ;
#66062=VECTOR ( 'NONE', #52858, 1000.000000000000000 ) ;
#66095=VECTOR ( 'NONE', #1309, 1000.000000000000000 ) ;
#66104=DIRECTION ( 'NONE',  ( 1.000000000000000000, 0.000000000000000000, 0.000000000000000000 ) ) ;
#66124=CIRCLE ( 'NONE', #9670, 1.000000000000001776 ) ;
#66220=ORIENTED_EDGE ( 'NONE', *, *, #35912, .F. ) ;
#66239=DIRECTION ( 'NONE',  ( 0.000000000000000000, 0.000000000000000000, 1.000000000000000000 ) ) ;
#66308=VECTOR ( 'NONE', #64556, 1000.000000000000000 ) ;
#66315=EDGE_CURVE ( 'NONE', #63045, #17547, #39947, .T. ) ;
#66443=ORIENTED_EDGE ( 'NONE', *, *, #6684, .T. ) ;
#66458=CARTESIAN_POINT ( 'NONE',  ( -11.18999999999999950, 12.00000000000000178, -5.000000000000000000 ) ) ;
#66466=CIRCLE ( 'NONE', #58568, 0.7499999999999997780 ) ;
#66577=ADVANCED_FACE ( 'NONE', ( #5026, #37213 ), #25556, .T. ) ;
#66614=EDGE_CURVE ( 'NONE', #38962, #36500, #52401, .T. ) ;
#66668=DIRECTION ( 'NONE',  ( 0.000000000000000000, 0.000000000000000000, 1.000000000000000000 ) ) ;
#66680=CARTESIAN_POINT ( 'NONE',  ( 8.249999999999996447, 8.250000000000001776, -5.000000000000000000 ) ) ;
#66701=EDGE_CURVE ( 'NONE', #34737, #4189, #15644, .T. ) ;
#66773=DIRECTION ( 'NONE',  ( 1.000000000000000000, 0.000000000000000000, 0.000000000000000000 ) ) ;
#66894=DIRECTION ( 'NONE',  ( 0.000000000000000000, 0.000000000000000000, -1.000000000000000000 ) ) ;
#66909=ORIENTED_EDGE ( 'NONE', *, *, #345, .F. ) ;
#66958=VECTOR ( 'NONE', #64786, 1000.000000000000000 ) ;
#66999=DIRECTION ( 'NONE',  ( -1.000000000000000000, -1.084202172485504434E-16, 0.000000000000000000 ) ) ;
#67055=VECTOR ( 'NONE', #65023, 1000.000000000000000 ) ;
#67081=CARTESIAN_POINT ( 'NONE',  ( -8.000000000000000000, -8.000000000000000000, 0.000000000000000000 ) ) ;
#67118=VECTOR ( 'NONE', #43888, 1000.000000000000000 ) ;
#67127=EDGE_LOOP ( 'NONE', ( #42867, #54071, #3655, #30458, #14323, #25996 ) ) ;
#67251=EDGE_CURVE ( 'NONE', #56996, #15758, #36702, .T. ) ;
#67294=CARTESIAN_POINT ( 'NONE',  ( 7.261609891743268541, -8.000000000000000000, -1.000000000000000000 ) ) ;
#67365=CARTESIAN_POINT ( 'NONE',  ( -11.18999999999999950, 12.00000000000000000, -4.250000000000000000 ) ) ;
#67573=ORIENTED_EDGE ( 'NONE', *, *, #2170, .T. ) ;
#67890=VERTEX_POINT ( 'NONE', #18764 ) ;
#67953=EDGE_LOOP ( 'NONE', ( #59493, #44851, #65562, #34562 ) ) ;
#67955=DIRECTION ( 'NONE',  ( 1.000000000000000000, 0.000000000000000000, 0.000000000000000000 ) ) ;
#67959=EDGE_CURVE ( 'NONE', #18593, #21803, #47737, .T. ) ;
#67977=CIRCLE ( 'NONE', #14939, 0.7499999999999997780 ) ;
#68033=ORIENTED_EDGE ( 'NONE', *, *, #29934, .F. ) ;
#68058=DIRECTION ( 'NONE',  ( 0.000000000000000000, -1.000000000000000000, 0.000000000000000000 ) ) ;
#68089=STYLED_ITEM ( 'NONE', ( #31388 ), #65930 ) ;
#68148=CARTESIAN_POINT ( 'NONE',  ( 8.249999999999996447, 8.250000000000001776, 0.000000000000000000 ) ) ;
#68176=DIRECTION ( 'NONE',  ( 1.000000000000000000, -0.000000000000000000, 0.000000000000000000 ) ) ;
#68290=EDGE_LOOP ( 'NONE', ( #38800, #23117, #16415, #16561 ) ) ;
#68339=CIRCLE ( 'NONE', #60392, 0.7499999999999997780 ) ;
#68347=ORIENTED_EDGE ( 'NONE', *, *, #32449, .T. ) ;
#68392=ADVANCED_FACE ( 'NONE', ( #51561 ), #35991, .T. ) ;
#68440=AXIS2_PLACEMENT_3D ( 'NONE', #17750, #18422, #1827 ) ;
#68485=CARTESIAN_POINT ( 'NONE',  ( -8.000000000000000000, -6.879816696376141572, 5.000000000000000000 ) ) ;
#68773=DIRECTION ( 'NONE',  ( 0.000000000000000000, 0.000000000000000000, 1.000000000000000000 ) ) ;
#68998=CARTESIAN_POINT ( 'NONE',  ( -12.00000000000000178, -11.18999999999999950, -4.250000000000000000 ) ) ;
#69007=LINE ( 'NONE', #55179, #16021 ) ;
#69129=ORIENTED_EDGE ( 'NONE', *, *, #32382, .T. ) ;
#69146=UNCERTAINTY_MEASURE_WITH_UNIT (LENGTH_MEASURE( 1.000000000000000082E-05 ), #23113, 'distance_accuracy_value', 'NONE');
#69273=CARTESIAN_POINT ( 'NONE',  ( -12.00000000000000000, 11.18999999999999950, 0.000000000000000000 ) ) ;
#69275=ORIENTED_EDGE ( 'NONE', *, *, #59592, .F. ) ;
#69278=ORIENTED_EDGE ( 'NONE', *, *, #67251, .F. ) ;
#69298=EDGE_CURVE ( 'NONE', #22012, #53008, #35829, .T. ) ;
#69375=CARTESIAN_POINT ( 'NONE',  ( -8.249999999999996447, -7.848062532927998269, -5.000000000000000000 ) ) ;
#69406=DIRECTION ( 'NONE',  ( 1.000000000000000000, 0.000000000000000000, 0.000000000000000000 ) ) ;
#69453=CYLINDRICAL_SURFACE ( 'NONE', #38120, 0.7499999999999997780 ) ;
#69460=DIRECTION ( 'NONE',  ( -7.751221965937476285E-17, -1.000000000000000000, 0.000000000000000000 ) ) ;
#69696=DIRECTION ( 'NONE',  ( 0.000000000000000000, 0.000000000000000000, 1.000000000000000000 ) ) ;
#69731=AXIS2_PLACEMENT_3D ( 'NONE', #48038, #37436, #58996 ) ;
#69825=DIRECTION ( 'NONE',  ( 0.000000000000000000, 0.000000000000000000, 1.000000000000000000 ) ) ;
#69869=LINE ( 'NONE', #68485, #11341 ) ;
#69971=DIRECTION ( 'NONE',  ( -1.000000000000000000, 0.000000000000000000, 0.000000000000000000 ) ) ;
ENDSEC;
END-ISO-10303-21;
